ISO-10303-21;
HEADER;
FILE_DESCRIPTION (('STEP AP214'),
    '1' );
FILE_NAME ('Top Metal Cover Plate.step',
    '2026-10-09T19:32:29',
    ( '' ),
    ( '' ),
    'SwSTEP 2.0',
    'SolidWorks 2026',
    '' );
FILE_SCHEMA (( 'AUTOMOTIVE_DESIGN' ));
ENDSEC;

DATA;
#15=EDGE_LOOP ( 'NONE', ( #13196, #1670, #3615, #581 ) ) ;
#16=CYLINDRICAL_SURFACE ( 'NONE', #2043, 0.04999999999999969746 ) ;
#34=EDGE_CURVE ( 'NONE', #13183, #12938, #7797, .T. ) ;
#62=ORIENTED_EDGE ( 'NONE', *, *, #5567, .F. ) ;
#84=VERTEX_POINT ( 'NONE', #15129 ) ;
#86=EDGE_CURVE ( 'NONE', #1835, #616, #17602, .T. ) ;
#90=EDGE_CURVE ( 'NONE', #4403, #2448, #5018, .T. ) ;
#108=EDGE_CURVE ( 'NONE', #9178, #84, #9359, .T. ) ;
#141=ORIENTED_EDGE ( 'NONE', *, *, #4492, .T. ) ;
#148=EDGE_CURVE ( 'NONE', #7436, #747, #4086, .T. ) ;
#169=VECTOR ( 'NONE', #1507, 1000.000000000000000 ) ;
#183=ORIENTED_EDGE ( 'NONE', *, *, #8245, .T. ) ;
#187=EDGE_CURVE ( 'NONE', #1492, #1173, #8443, .T. ) ;
#193=CARTESIAN_POINT ( 'NONE',  ( -1.149999999999999911, 9.248236190979499227, 7.693185165257809821 ) ) ;
#195=CARTESIAN_POINT ( 'NONE',  ( 1.899999999999999911, 0.5999999999999999778, 6.599999999999999645 ) ) ;
#197=CLOSED_SHELL ( 'NONE', ( #3822, #8083, #11142, #1743, #2496, #9758, #12462, #15962, #6872, #9484, #17524, #17256, #4961, #15462, #764, #3248, #10059, #5969, #10152, #4929, #18252, #3273, #16322, #10513, #3922, #2712, #13996, #6295, #532, #11967, #9528, #2422, #10741, #3839, #15384, #3945, #14577, #1473, #15447, #8798, #14553, #6473, #731, #10373, #15290, #13653, #3441, #1008, #14533, #415, #7664, #14234 ) ) ;
#215=EDGE_CURVE ( 'NONE', #1195, #3917, #16867, .T. ) ;
#230=DIRECTION ( 'NONE',  ( -1.000000000000000000, 1.224646799147350002E-16, 0.000000000000000000 ) ) ;
#245=CARTESIAN_POINT ( 'NONE',  ( 1.750000000000000000, 11.40000000000000036, 7.700000000000000178 ) ) ;
#267=ORIENTED_EDGE ( 'NONE', *, *, #17989, .T. ) ;
#270=( NAMED_UNIT ( * ) PLANE_ANGLE_UNIT ( ) SI_UNIT ( $, .RADIAN. ) );
#271=DIRECTION ( 'NONE',  ( -1.000000000000000000, 3.700743415417179758E-16, 0.000000000000000000 ) ) ;
#280=DIRECTION ( 'NONE',  ( 1.850371707708589879E-16, 1.000000000000000000, 0.000000000000000000 ) ) ;
#295=FILL_AREA_STYLE_COLOUR ( '', #15889 ) ;
#303=AXIS2_PLACEMENT_3D ( 'NONE', #18184, #4318, #5723 ) ;
#324=EDGE_CURVE ( 'NONE', #84, #12938, #3836, .T. ) ;
#357=CARTESIAN_POINT ( 'NONE',  ( -1.149999999999999911, 9.274118095489749081, 7.596592582628910684 ) ) ;
#381=( NAMED_UNIT ( * ) SI_UNIT ( $, .STERADIAN. ) SOLID_ANGLE_UNIT ( ) );
#393=ORIENTED_EDGE ( 'NONE', *, *, #5976, .T. ) ;
#404=VERTEX_POINT ( 'NONE', #1430 ) ;
#408=CARTESIAN_POINT ( 'NONE',  ( 1.750000000000000000, 0.5999999999999999778, 7.700000000000000178 ) ) ;
#415=ADVANCED_FACE ( 'NONE', ( #12730 ), #3243, .T. ) ;
#422=DIRECTION ( 'NONE',  ( 0.000000000000000000, 0.000000000000000000, 1.000000000000000000 ) ) ;
#430=VECTOR ( 'NONE', #9262, 1000.000000000000000 ) ;
#443=CARTESIAN_POINT ( 'NONE',  ( -1.750000000000000000, 0.5999999999999999778, 7.700000000000000178 ) ) ;
#456=CARTESIAN_POINT ( 'NONE',  ( -1.699999999999999956, 9.299999999999998934, 7.599999999999999645 ) ) ;
#462=CARTESIAN_POINT ( 'NONE',  ( 1.750000000000000000, 11.40000000000000036, 7.599999999999999645 ) ) ;
#482=AXIS2_PLACEMENT_3D ( 'NONE', #15870, #14482, #11517 ) ;
#493=EDGE_LOOP ( 'NONE', ( #3979, #4841, #1424, #2607 ) ) ;
#522=ORIENTED_EDGE ( 'NONE', *, *, #6504, .F. ) ;
#532=ADVANCED_FACE ( 'NONE', ( #12413 ), #10936, .F. ) ;
#533=LINE ( 'NONE', #14427, #12662 ) ;
#562=FACE_OUTER_BOUND ( 'NONE', #15, .T. ) ;
#581=ORIENTED_EDGE ( 'NONE', *, *, #8066, .F. ) ;
#597=ORIENTED_EDGE ( 'NONE', *, *, #12740, .F. ) ;
#616=VERTEX_POINT ( 'NONE', #16849 ) ;
#618=PLANE ( 'NONE',  #12952 ) ;
#624=DIRECTION ( 'NONE',  ( 1.000000000000000000, 0.000000000000000000, 0.000000000000000000 ) ) ;
#629=CARTESIAN_POINT ( 'NONE',  ( 1.110223024625159893E-15, 0.3264109415988649676, 5.199061676633699669 ) ) ;
#639=EDGE_CURVE ( 'NONE', #9659, #10455, #8614, .T. ) ;
#650=DIRECTION ( 'NONE',  ( 1.000000000000000000, 0.000000000000000000, 0.000000000000000000 ) ) ;
#688=DIRECTION ( 'NONE',  ( -1.000000000000000000, 1.224646799147350002E-16, 0.000000000000000000 ) ) ;
#692=DIRECTION ( 'NONE',  ( 3.700743415417190112E-16, 1.000000000000000000, 0.000000000000000000 ) ) ;
#693=FACE_BOUND ( 'NONE', #4148, .T. ) ;
#695=ORIENTED_EDGE ( 'NONE', *, *, #1552, .T. ) ;
#731=ADVANCED_FACE ( 'NONE', ( #17191 ), #1295, .F. ) ;
#745=LINE ( 'NONE', #12048, #16067 ) ;
#747=VERTEX_POINT ( 'NONE', #8341 ) ;
#748=EDGE_LOOP ( 'NONE', ( #6942, #11211, #13896, #14594, #10227, #13721, #1763, #3427, #3347, #8912, #16607, #3116, #1632, #10771, #8081, #10005 ) ) ;
#754=EDGE_CURVE ( 'NONE', #2115, #2289, #6939, .T. ) ;
#760=EDGE_CURVE ( 'NONE', #2828, #7698, #4894, .T. ) ;
#764=ADVANCED_FACE ( 'NONE', ( #4594 ), #2377, .T. ) ;
#775=ORIENTED_EDGE ( 'NONE', *, *, #17107, .T. ) ;
#784=AXIS2_PLACEMENT_3D ( 'NONE', #4287, #7263, #3090 ) ;
#790=ORIENTED_EDGE ( 'NONE', *, *, #5174, .T. ) ;
#796=VERTEX_POINT ( 'NONE', #890 ) ;
#800=VECTOR ( 'NONE', #5463, 1000.000000000000000 ) ;
#811=CIRCLE ( 'NONE', #6130, 0.1499999999999999667 ) ;
#827=PLANE ( 'NONE',  #9362 ) ;
#830=APPLICATION_CONTEXT ( 'automotive_design' ) ;
#850=ORIENTED_EDGE ( 'NONE', *, *, #14353, .T. ) ;
#854=ORIENTED_EDGE ( 'NONE', *, *, #7368, .F. ) ;
#865=ORIENTED_EDGE ( 'NONE', *, *, #17396, .T. ) ;
#887=DIRECTION ( 'NONE',  ( 0.000000000000000000, 0.000000000000000000, -1.000000000000000000 ) ) ;
#890=CARTESIAN_POINT ( 'NONE',  ( 0.2750000000000004663, 2.299999999999999822, 7.700000000000000178 ) ) ;
#901=ORIENTED_EDGE ( 'NONE', *, *, #754, .F. ) ;
#906=ORIENTED_EDGE ( 'NONE', *, *, #4194, .T. ) ;
#911=CARTESIAN_POINT ( 'NONE',  ( -1.800000000000000044, 3.552713678800499647E-16, 9.441371669411539713 ) ) ;
#927=DIRECTION ( 'NONE',  ( 7.656710514656250048E-17, -0.9659258262890690894, -0.2588190451025180749 ) ) ;
#942=DIRECTION ( 'NONE',  ( -1.850371707708589879E-16, 1.000000000000000000, 0.000000000000000000 ) ) ;
#943=DIRECTION ( 'NONE',  ( 1.000000000000000000, 0.000000000000000000, 0.000000000000000000 ) ) ;
#972=DIRECTION ( 'NONE',  ( 2.220446049250309876E-16, 1.000000000000000000, 1.479114197289400113E-30 ) ) ;
#975=FACE_OUTER_BOUND ( 'NONE', #1124, .T. ) ;
#990=CARTESIAN_POINT ( 'NONE',  ( 1.699999999999999956, 9.299999999999998934, 7.599999999999999645 ) ) ;
#1008=ADVANCED_FACE ( 'NONE', ( #15154 ), #13845, .T. ) ;
#1017=PLANE ( 'NONE',  #2330 ) ;
#1024=DIRECTION ( 'NONE',  ( -1.903239470785979823E-16, -1.000000000000000000, 0.000000000000000000 ) ) ;
#1033=CARTESIAN_POINT ( 'NONE',  ( -1.149999999999999911, 9.274118095489749081, 7.596592582628910684 ) ) ;
#1050=EDGE_LOOP ( 'NONE', ( #10330, #2699, #7996, #1910 ) ) ;
#1082=ORIENTED_EDGE ( 'NONE', *, *, #1809, .T. ) ;
#1121=CARTESIAN_POINT ( 'NONE',  ( 1.899999999999999911, 6.661338147750959950E-17, 9.441371669411539713 ) ) ;
#1124=EDGE_LOOP ( 'NONE', ( #2346, #17137, #10697, #13392 ) ) ;
#1126=CARTESIAN_POINT ( 'NONE',  ( 0.5999999999999999778, 0.5999999999999999778, 7.599999999999999645 ) ) ;
#1135=DIRECTION ( 'NONE',  ( -1.000000000000000000, 0.000000000000000000, 0.000000000000000000 ) ) ;
#1162=AXIS2_PLACEMENT_3D ( 'NONE', #13573, #887, #8023 ) ;
#1166=DIRECTION ( 'NONE',  ( 0.000000000000000000, -1.000000000000000000, -8.934339325041029556E-19 ) ) ;
#1173=VERTEX_POINT ( 'NONE', #3930 ) ;
#1195=VERTEX_POINT ( 'NONE', #15243 ) ;
#1222=PRODUCT_DEFINITION_SHAPE ( 'NONE', 'NONE',  #7122 ) ;
#1228=DIRECTION ( 'NONE',  ( 0.000000000000000000, -0.2588190451025150218, 0.9659258262890698665 ) ) ;
#1250=DIRECTION ( 'NONE',  ( -5.551115123125880521E-15, 1.000000000000000000, 6.055990775824630636E-30 ) ) ;
#1273=DIRECTION ( 'NONE',  ( -1.000000000000000000, 0.000000000000000000, 0.000000000000000000 ) ) ;
#1280=FACE_OUTER_BOUND ( 'NONE', #5828, .T. ) ;
#1281=DIRECTION ( 'NONE',  ( -1.000000000000000000, 0.000000000000000000, 0.000000000000000000 ) ) ;
#1295=PLANE ( 'NONE',  #13490 ) ;
#1297=LINE ( 'NONE', #2509, #9090 ) ;
#1301=ORIENTED_EDGE ( 'NONE', *, *, #4407, .T. ) ;
#1304=ORIENTED_EDGE ( 'NONE', *, *, #17396, .F. ) ;
#1310=DIRECTION ( 'NONE',  ( -2.055968564120659776E-16, -1.000000000000000000, 0.000000000000000000 ) ) ;
#1318=CARTESIAN_POINT ( 'NONE',  ( 1.800000000000000044, 11.40000000000000036, 6.599999999999999645 ) ) ;
#1319=ORIENTED_EDGE ( 'NONE', *, *, #11624, .T. ) ;
#1328=EDGE_CURVE ( 'NONE', #14407, #3917, #8228, .T. ) ;
#1352=LINE ( 'NONE', #11168, #11141 ) ;
#1368=DIRECTION ( 'NONE',  ( 0.000000000000000000, 0.000000000000000000, -1.000000000000000000 ) ) ;
#1369=LINE ( 'NONE', #7032, #17082 ) ;
#1376=CARTESIAN_POINT ( 'NONE',  ( -1.699999999999999956, 2.299999999999999822, 7.599999999999999645 ) ) ;
#1382=AXIS2_PLACEMENT_3D ( 'NONE', #5481, #2799, #16771 ) ;
#1396=PRODUCT_DEFINITION_CONTEXT ( 'detailed design', #6861, 'design' ) ;
#1401=CARTESIAN_POINT ( 'NONE',  ( -1.300000000000000044, 0.000000000000000000, 7.599999999999999645 ) ) ;
#1416=CARTESIAN_POINT ( 'NONE',  ( 1.149999999999999911, 9.274118095489749081, 7.596592582628910684 ) ) ;
#1420=AXIS2_PLACEMENT_3D ( 'NONE', #911, #2006, #6550 ) ;
#1424=ORIENTED_EDGE ( 'NONE', *, *, #1476, .T. ) ;
#1428=VECTOR ( 'NONE', #3053, 1000.000000000000000 ) ;
#1430=CARTESIAN_POINT ( 'NONE',  ( -1.699999999999999956, 2.299999999999999822, 7.599999999999999645 ) ) ;
#1433=VECTOR ( 'NONE', #2358, 1000.000000000000000 ) ;
#1435=DIRECTION ( 'NONE',  ( 1.000000000000000000, 0.000000000000000000, 0.000000000000000000 ) ) ;
#1436=DIRECTION ( 'NONE',  ( -1.000000000000000000, 2.220446049250309876E-16, 0.000000000000000000 ) ) ;
#1448=ORIENTED_EDGE ( 'NONE', *, *, #2634, .F. ) ;
#1460=DIRECTION ( 'NONE',  ( 0.000000000000000000, 0.000000000000000000, -1.000000000000000000 ) ) ;
#1473=ADVANCED_FACE ( 'NONE', ( #1280 ), #12570, .T. ) ;
#1476=EDGE_CURVE ( 'NONE', #16779, #1993, #10429, .T. ) ;
#1478=PRODUCT_DEFINITION_FORMATION_WITH_SPECIFIED_SOURCE ( 'ANY', '', #5367, .NOT_KNOWN. ) ;
#1492=VERTEX_POINT ( 'NONE', #4317 ) ;
#1495=EDGE_CURVE ( 'NONE', #2828, #5745, #9981, .T. ) ;
#1496=FACE_OUTER_BOUND ( 'NONE', #9801, .T. ) ;
#1507=DIRECTION ( 'NONE',  ( 2.055968564120659776E-16, 1.000000000000000000, 0.000000000000000000 ) ) ;
#1508=DIRECTION ( 'NONE',  ( 0.7071067811865470176, -0.7071067811865480168, 0.000000000000000000 ) ) ;
#1548=DIRECTION ( 'NONE',  ( 0.000000000000000000, 0.000000000000000000, 1.000000000000000000 ) ) ;
#1552=EDGE_CURVE ( 'NONE', #747, #4341, #7204, .T. ) ;
#1559=DIRECTION ( 'NONE',  ( 1.000000000000000000, 0.000000000000000000, 0.000000000000000000 ) ) ;
#1562=EDGE_LOOP ( 'NONE', ( #2488, #15250 ) ) ;
#1565=CARTESIAN_POINT ( 'NONE',  ( 0.5999999999999999778, 11.40000000000000036, 7.599999999999999645 ) ) ;
#1583=DIRECTION ( 'NONE',  ( 0.000000000000000000, 0.000000000000000000, 1.000000000000000000 ) ) ;
#1584=ORIENTED_EDGE ( 'NONE', *, *, #13908, .T. ) ;
#1594=DIRECTION ( 'NONE',  ( -8.269460797427580527E-16, 0.000000000000000000, 1.000000000000000000 ) ) ;
#1599=CARTESIAN_POINT ( 'NONE',  ( -1.800000000000000044, 0.5999999999999999778, 6.599999999999999645 ) ) ;
#1617=ORIENTED_EDGE ( 'NONE', *, *, #12083, .T. ) ;
#1618=EDGE_CURVE ( 'NONE', #1835, #3272, #11543, .T. ) ;
#1632=ORIENTED_EDGE ( 'NONE', *, *, #6290, .T. ) ;
#1645=EDGE_LOOP ( 'NONE', ( #6162, #8005, #2854, #8704 ) ) ;
#1663=VERTEX_POINT ( 'NONE', #10418 ) ;
#1665=EDGE_CURVE ( 'NONE', #10455, #4443, #7648, .T. ) ;
#1670=ORIENTED_EDGE ( 'NONE', *, *, #5013, .F. ) ;
#1706=PLANE ( 'NONE',  #482 ) ;
#1709=AXIS2_PLACEMENT_3D ( 'NONE', #7640, #1978, #11621 ) ;
#1736=AXIS2_PLACEMENT_3D ( 'NONE', #2727, #12529, #18142 ) ;
#1742=ORIENTED_EDGE ( 'NONE', *, *, #3121, .F. ) ;
#1743=ADVANCED_FACE ( 'NONE', ( #3302 ), #17353, .T. ) ;
#1746=( LENGTH_UNIT ( ) NAMED_UNIT ( * ) SI_UNIT ( .MILLI., .METRE. ) );
#1760=LINE ( 'NONE', #14260, #16505 ) ;
#1763=ORIENTED_EDGE ( 'NONE', *, *, #9516, .T. ) ;
#1767=AXIS2_PLACEMENT_3D ( 'NONE', #14108, #8469, #1436 ) ;
#1775=CARTESIAN_POINT ( 'NONE',  ( 1.899999999999999911, 0.5999999999999999778, 7.599999999999999645 ) ) ;
#1776=CARTESIAN_POINT ( 'NONE',  ( 1.800000000000000044, 11.40000000000000036, 7.550000000000000711 ) ) ;
#1809=EDGE_CURVE ( 'NONE', #9985, #14961, #5402, .T. ) ;
#1812=ORIENTED_EDGE ( 'NONE', *, *, #1495, .F. ) ;
#1823=CARTESIAN_POINT ( 'NONE',  ( -0.5999999999999999778, 0.5999999999999999778, 7.599999999999999645 ) ) ;
#1835=VERTEX_POINT ( 'NONE', #6793 ) ;
#1848=PLANE ( 'NONE',  #7110 ) ;
#1872=DIRECTION ( 'NONE',  ( 0.000000000000000000, 0.000000000000000000, 1.000000000000000000 ) ) ;
#1877=DIRECTION ( 'NONE',  ( -1.224646799147350002E-16, -1.000000000000000000, 0.000000000000000000 ) ) ;
#1887=EDGE_CURVE ( 'NONE', #17150, #7174, #10459, .T. ) ;
#1910=ORIENTED_EDGE ( 'NONE', *, *, #12209, .F. ) ;
#1937=CARTESIAN_POINT ( 'NONE',  ( 1.699999999999999956, 2.299999999999999822, 7.599999999999999645 ) ) ;
#1964=MECHANICAL_DESIGN_GEOMETRIC_PRESENTATION_REPRESENTATION('',(#9672),#16767);
#1978=DIRECTION ( 'NONE',  ( 0.000000000000000000, 1.000000000000000000, -1.836189155707839943E-31 ) ) ;
#1993=VERTEX_POINT ( 'NONE', #5747 ) ;
#1997=CARTESIAN_POINT ( 'NONE',  ( -1.750000000000000000, 0.5999999999999999778, 7.599999999999999645 ) ) ;
#2006=DIRECTION ( 'NONE',  ( -1.000000000000000000, 2.220446049250309876E-16, -8.269460797427580527E-16 ) ) ;
#2018=ORIENTED_EDGE ( 'NONE', *, *, #6290, .F. ) ;
#2028=DIRECTION ( 'NONE',  ( 1.000000000000000000, 0.000000000000000000, 0.000000000000000000 ) ) ;
#2043=AXIS2_PLACEMENT_3D ( 'NONE', #13979, #15669, #1583 ) ;
#2064=EDGE_CURVE ( 'NONE', #9178, #2115, #4789, .T. ) ;
#2089=ORIENTED_EDGE ( 'NONE', *, *, #11703, .T. ) ;
#2108=DIRECTION ( 'NONE',  ( 0.000000000000000000, -0.2588190451025161321, 0.9659258262890695335 ) ) ;
#2115=VERTEX_POINT ( 'NONE', #2213 ) ;
#2123=ORIENTED_EDGE ( 'NONE', *, *, #12897, .T. ) ;
#2146=SHAPE_REPRESENTATION ( 'Top Metal Cover Plate', ( #17681 ), #3818 ) ;
#2166=VECTOR ( 'NONE', #5635, 1000.000000000000000 ) ;
#2191=EDGE_CURVE ( 'NONE', #8647, #17150, #8329, .T. ) ;
#2213=CARTESIAN_POINT ( 'NONE',  ( -0.9499999999999999556, 2.299999999999999822, 7.700000000000000178 ) ) ;
#2236=ORIENTED_EDGE ( 'NONE', *, *, #9045, .T. ) ;
#2238=DIRECTION ( 'NONE',  ( -7.656710514656250048E-17, 0.9659258262890690894, 0.2588190451025180749 ) ) ;
#2254=VECTOR ( 'NONE', #5654, 1000.000000000000000 ) ;
#2264=CARTESIAN_POINT ( 'NONE',  ( 1.750000000000000000, 11.40000000000000036, 7.700000000000000178 ) ) ;
#2281=AXIS2_PLACEMENT_3D ( 'NONE', #11073, #3857, #13858 ) ;
#2289=VERTEX_POINT ( 'NONE', #5098 ) ;
#2292=CIRCLE ( 'NONE', #2581, 0.2750000000000000222 ) ;
#2300=VECTOR ( 'NONE', #15013, 1000.000000000000114 ) ;
#2302=CARTESIAN_POINT ( 'NONE',  ( 1.149999999999999911, 9.274118095489749081, 7.596592582628910684 ) ) ;
#2313=DIRECTION ( 'NONE',  ( -1.000000000000000000, 0.000000000000000000, 0.000000000000000000 ) ) ;
#2316=DIRECTION ( 'NONE',  ( 0.000000000000000000, 0.000000000000000000, 1.000000000000000000 ) ) ;
#2319=AXIS2_PLACEMENT_3D ( 'NONE', #4785, #6269, #16097 ) ;
#2322=VECTOR ( 'NONE', #692, 1000.000000000000000 ) ;
#2330=AXIS2_PLACEMENT_3D ( 'NONE', #16469, #5372, #3784 ) ;
#2342=CARTESIAN_POINT ( 'NONE',  ( 0.5999999999999999778, 10.80000000000000071, 7.599999999999999645 ) ) ;
#2346=ORIENTED_EDGE ( 'NONE', *, *, #7368, .T. ) ;
#2350=EDGE_CURVE ( 'NONE', #10455, #2720, #16306, .T. ) ;
#2358=DIRECTION ( 'NONE',  ( 0.000000000000000000, 0.000000000000000000, 1.000000000000000000 ) ) ;
#2369=EDGE_CURVE ( 'NONE', #13468, #7602, #7784, .T. ) ;
#2377=PLANE ( 'NONE',  #12009 ) ;
#2379=EDGE_CURVE ( 'NONE', #16402, #8925, #745, .T. ) ;
#2389=ORIENTED_EDGE ( 'NONE', *, *, #5298, .F. ) ;
#2422=ADVANCED_FACE ( 'NONE', ( #15020 ), #12235, .T. ) ;
#2433=LINE ( 'NONE', #8078, #16668 ) ;
#2440=DIRECTION ( 'NONE',  ( 0.000000000000000000, 0.000000000000000000, 1.000000000000000000 ) ) ;
#2448=VERTEX_POINT ( 'NONE', #10842 ) ;
#2452=EDGE_CURVE ( 'NONE', #17576, #3272, #2433, .T. ) ;
#2464=ORIENTED_EDGE ( 'NONE', *, *, #7104, .T. ) ;
#2484=DIRECTION ( 'NONE',  ( 0.000000000000000000, -1.000000000000000000, 0.000000000000000000 ) ) ;
#2487=DIRECTION ( 'NONE',  ( 1.000000000000000000, 0.000000000000000000, 0.000000000000000000 ) ) ;
#2488=ORIENTED_EDGE ( 'NONE', *, *, #760, .T. ) ;
#2496=ADVANCED_FACE ( 'NONE', ( #1496 ), #7228, .F. ) ;
#2499=DIRECTION ( 'NONE',  ( -0.7071067811865475727, -0.7071067811865475727, 0.000000000000000000 ) ) ;
#2509=CARTESIAN_POINT ( 'NONE',  ( 1.899999999999999911, 0.5999999999999999778, 7.599999999999999645 ) ) ;
#2511=ORIENTED_EDGE ( 'NONE', *, *, #14365, .F. ) ;
#2524=CARTESIAN_POINT ( 'NONE',  ( 1.149999999999999911, 9.299999999999998934, 7.500000000000000000 ) ) ;
#2535=ORIENTED_EDGE ( 'NONE', *, *, #2695, .F. ) ;
#2538=FACE_OUTER_BOUND ( 'NONE', #14728, .T. ) ;
#2551=VECTOR ( 'NONE', #6022, 1000.000000000000000 ) ;
#2562=CIRCLE ( 'NONE', #784, 0.1000000000000002554 ) ;
#2579=VECTOR ( 'NONE', #1024, 1000.000000000000000 ) ;
#2581=AXIS2_PLACEMENT_3D ( 'NONE', #17030, #4355, #8357 ) ;
#2586=ORIENTED_EDGE ( 'NONE', *, *, #15498, .T. ) ;
#2605=AXIS2_PLACEMENT_3D ( 'NONE', #17369, #4587, #10160 ) ;
#2607=ORIENTED_EDGE ( 'NONE', *, *, #14345, .F. ) ;
#2611=VERTEX_POINT ( 'NONE', #16460 ) ;
#2634=EDGE_CURVE ( 'NONE', #10238, #11655, #12124, .T. ) ;
#2655=ORIENTED_EDGE ( 'NONE', *, *, #14959, .T. ) ;
#2692=VERTEX_POINT ( 'NONE', #11598 ) ;
#2695=EDGE_CURVE ( 'NONE', #1663, #2916, #10468, .T. ) ;
#2699=ORIENTED_EDGE ( 'NONE', *, *, #5174, .F. ) ;
#2701=UNCERTAINTY_MEASURE_WITH_UNIT (LENGTH_MEASURE( 1.000000000000000082E-05 ), #6020, 'distance_accuracy_value', 'NONE');
#2703=EDGE_LOOP ( 'NONE', ( #8993, #13075, #15401, #10126 ) ) ;
#2712=ADVANCED_FACE ( 'NONE', ( #11033 ), #6388, .T. ) ;
#2715=LINE ( 'NONE', #1599, #3175 ) ;
#2720=VERTEX_POINT ( 'NONE', #3989 ) ;
#2726=ORIENTED_EDGE ( 'NONE', *, *, #11703, .F. ) ;
#2727=CARTESIAN_POINT ( 'NONE',  ( 3.371799150351489833E-16, 2.299999999999999822, 7.700000000000000178 ) ) ;
#2789=ORIENTED_EDGE ( 'NONE', *, *, #8245, .F. ) ;
#2799=DIRECTION ( 'NONE',  ( 0.000000000000000000, 0.000000000000000000, -1.000000000000000000 ) ) ;
#2828=VERTEX_POINT ( 'NONE', #6391 ) ;
#2837=ORIENTED_EDGE ( 'NONE', *, *, #17107, .F. ) ;
#2854=ORIENTED_EDGE ( 'NONE', *, *, #8846, .T. ) ;
#2860=VERTEX_POINT ( 'NONE', #16053 ) ;
#2889=CARTESIAN_POINT ( 'NONE',  ( -1.899999999999999911, 3.774758283725530167E-16, 9.441371669411539713 ) ) ;
#2898=AXIS2_PLACEMENT_3D ( 'NONE', #2889, #4258, #1594 ) ;
#2916=VERTEX_POINT ( 'NONE', #16603 ) ;
#2925=DIRECTION ( 'NONE',  ( -1.000000000000000000, 0.000000000000000000, 0.000000000000000000 ) ) ;
#2949=ORIENTED_EDGE ( 'NONE', *, *, #17956, .T. ) ;
#2977=ORIENTED_EDGE ( 'NONE', *, *, #2369, .F. ) ;
#2982=DIRECTION ( 'NONE',  ( -2.055968564120659776E-16, -1.000000000000000000, 0.000000000000000000 ) ) ;
#2990=FACE_OUTER_BOUND ( 'NONE', #11391, .T. ) ;
#2992=AXIS2_PLACEMENT_3D ( 'NONE', #8332, #9707, #1368 ) ;
#2997=DIRECTION ( 'NONE',  ( 1.000000000000000000, -2.220446049250309876E-16, 0.000000000000000000 ) ) ;
#3026=ORIENTED_EDGE ( 'NONE', *, *, #3366, .F. ) ;
#3031=EDGE_CURVE ( 'NONE', #10172, #2860, #5550, .T. ) ;
#3046=LINE ( 'NONE', #17460, #17066 ) ;
#3053=DIRECTION ( 'NONE',  ( 1.850371707708589879E-16, -1.000000000000000000, 0.000000000000000000 ) ) ;
#3056=AXIS2_PLACEMENT_3D ( 'NONE', #14047, #18183, #11089 ) ;
#3065=PRESENTATION_STYLE_ASSIGNMENT (( #15757 ) ) ;
#3090=DIRECTION ( 'NONE',  ( 0.000000000000000000, 0.000000000000000000, 1.000000000000000000 ) ) ;
#3102=EDGE_LOOP ( 'NONE', ( #10845, #13388, #5563, #11480 ) ) ;
#3116=ORIENTED_EDGE ( 'NONE', *, *, #5180, .T. ) ;
#3121=EDGE_CURVE ( 'NONE', #10238, #5712, #2715, .T. ) ;
#3123=FACE_OUTER_BOUND ( 'NONE', #3380, .T. ) ;
#3130=CARTESIAN_POINT ( 'NONE',  ( 0.2750000000000004663, 2.299999999999999822, 7.599999999999999645 ) ) ;
#3146=AXIS2_PLACEMENT_3D ( 'NONE', #12060, #17680, #2440 ) ;
#3175=VECTOR ( 'NONE', #4358, 1000.000000000000000 ) ;
#3197=EDGE_LOOP ( 'NONE', ( #10194, #6253, #7492, #4463 ) ) ;
#3198=VECTOR ( 'NONE', #13482, 1000.000000000000000 ) ;
#3218=CARTESIAN_POINT ( 'NONE',  ( 1.699999999999999956, 9.299999999999998934, 7.599999999999999645 ) ) ;
#3221=DIRECTION ( 'NONE',  ( -1.000000000000000000, -4.433365283261159518E-17, -1.187916647401989926E-17 ) ) ;
#3237=ORIENTED_EDGE ( 'NONE', *, *, #9596, .F. ) ;
#3243=PLANE ( 'NONE',  #9317 ) ;
#3245=DIRECTION ( 'NONE',  ( 1.000000000000000000, 0.000000000000000000, 0.000000000000000000 ) ) ;
#3248=ADVANCED_FACE ( 'NONE', ( #2990 ), #5581, .F. ) ;
#3254=LINE ( 'NONE', #13070, #9449 ) ;
#3260=EDGE_CURVE ( 'NONE', #6043, #8260, #4262, .T. ) ;
#3272=VERTEX_POINT ( 'NONE', #1775 ) ;
#3273=ADVANCED_FACE ( 'NONE', ( #562 ), #10450, .T. ) ;
#3294=CARTESIAN_POINT ( 'NONE',  ( 1.149999999999999911, 9.299999999999998934, 7.500000000000000000 ) ) ;
#3302=FACE_OUTER_BOUND ( 'NONE', #17486, .T. ) ;
#3307=CARTESIAN_POINT ( 'NONE',  ( -0.5999999999999999778, 7.347880794884128857E-17, 7.700000000000000178 ) ) ;
#3309=ORIENTED_EDGE ( 'NONE', *, *, #5048, .T. ) ;
#3310=DIRECTION ( 'NONE',  ( -4.433365283261159518E-17, 1.000000000000000000, 0.000000000000000000 ) ) ;
#3341=CARTESIAN_POINT ( 'NONE',  ( -0.5999999999999999778, 7.347880794884128857E-17, 7.599999999999999645 ) ) ;
#3346=DIRECTION ( 'NONE',  ( 2.261565420532729920E-16, 1.000000000000000000, 0.000000000000000000 ) ) ;
#3347=ORIENTED_EDGE ( 'NONE', *, *, #3260, .T. ) ;
#3366=EDGE_CURVE ( 'NONE', #616, #1663, #3745, .T. ) ;
#3368=LINE ( 'NONE', #8936, #15905 ) ;
#3380=EDGE_LOOP ( 'NONE', ( #13922, #7396, #3898, #1742 ) ) ;
#3381=CARTESIAN_POINT ( 'NONE',  ( 0.5999999999999999778, 11.40000000000000036, 7.599999999999999645 ) ) ;
#3384=ORIENTED_EDGE ( 'NONE', *, *, #18169, .T. ) ;
#3400=LINE ( 'NONE', #10644, #7069 ) ;
#3405=CARTESIAN_POINT ( 'NONE',  ( 1.699999999999999956, 9.299999999999998934, 7.700000000000000178 ) ) ;
#3427=ORIENTED_EDGE ( 'NONE', *, *, #14242, .T. ) ;
#3441=ADVANCED_FACE ( 'NONE', ( #17899, #5237, #6429 ), #4951, .T. ) ;
#3449=LINE ( 'NONE', #6321, #17314 ) ;
#3455=ORIENTED_EDGE ( 'NONE', *, *, #5902, .F. ) ;
#3463=CARTESIAN_POINT ( 'NONE',  ( 1.800000000000000044, 0.5999999999999999778, 7.550000000000000711 ) ) ;
#3478=VECTOR ( 'NONE', #6449, 1000.000000000000000 ) ;
#3484=CARTESIAN_POINT ( 'NONE',  ( 8.785293332290788772E-16, 10.80000000000000071, 7.599999999999999645 ) ) ;
#3486=CARTESIAN_POINT ( 'NONE',  ( 1.149999999999999911, 6.472933199251450276, 6.846017351831609865 ) ) ;
#3507=ORIENTED_EDGE ( 'NONE', *, *, #1665, .F. ) ;
#3511=EDGE_CURVE ( 'NONE', #17576, #6049, #12098, .T. ) ;
#3531=DIRECTION ( 'NONE',  ( 1.000000000000000000, 0.000000000000000000, 0.000000000000000000 ) ) ;
#3576=PLANE ( 'NONE',  #1420 ) ;
#3596=LINE ( 'NONE', #13229, #15002 ) ;
#3598=ORIENTED_EDGE ( 'NONE', *, *, #16143, .F. ) ;
#3603=DIRECTION ( 'NONE',  ( -2.220446049250309876E-16, -1.000000000000000000, -1.479114197289400113E-30 ) ) ;
#3615=ORIENTED_EDGE ( 'NONE', *, *, #12209, .T. ) ;
#3617=ORIENTED_EDGE ( 'NONE', *, *, #16825, .T. ) ;
#3639=CARTESIAN_POINT ( 'NONE',  ( 1.750000000000000000, 0.5999999999999999778, 7.700000000000000178 ) ) ;
#3651=CARTESIAN_POINT ( 'NONE',  ( 1.300000000000000044, -1.592040838891560081E-16, 7.599999999999999645 ) ) ;
#3682=ORIENTED_EDGE ( 'NONE', *, *, #12918, .F. ) ;
#3696=LINE ( 'NONE', #10745, #7910 ) ;
#3703=ORIENTED_EDGE ( 'NONE', *, *, #90, .T. ) ;
#3719=ORIENTED_EDGE ( 'NONE', *, *, #8897, .T. ) ;
#3740=DIRECTION ( 'NONE',  ( -1.048990684667790150E-15, 1.966625170870250139E-17, -1.000000000000000000 ) ) ;
#3745=LINE ( 'NONE', #3463, #6436 ) ;
#3747=VECTOR ( 'NONE', #17361, 1000.000000000000000 ) ;
#3753=PLANE ( 'NONE',  #18038 ) ;
#3769=CARTESIAN_POINT ( 'NONE',  ( -1.300000000000000044, 1.592040838891560081E-16, 7.700000000000000178 ) ) ;
#3771=ORIENTED_EDGE ( 'NONE', *, *, #34, .F. ) ;
#3784=DIRECTION ( 'NONE',  ( -1.850371707708589879E-16, -1.000000000000000000, 0.000000000000000000 ) ) ;
#3789=VECTOR ( 'NONE', #15857, 1000.000000000000000 ) ;
#3797=VECTOR ( 'NONE', #17158, 1000.000000000000000 ) ;
#3801=CARTESIAN_POINT ( 'NONE',  ( 1.300000000000000044, -1.592040838891560081E-16, 7.700000000000000178 ) ) ;
#3806=DIRECTION ( 'NONE',  ( 0.000000000000000000, -0.2588190451025180749, 0.9659258262890690894 ) ) ;
#3818=( GEOMETRIC_REPRESENTATION_CONTEXT ( 3 ) GLOBAL_UNCERTAINTY_ASSIGNED_CONTEXT ( ( #9551 ) ) GLOBAL_UNIT_ASSIGNED_CONTEXT ( ( #1746, #270, #12852 ) ) REPRESENTATION_CONTEXT ( 'NONE', 'WORKASPACE' ) );
#3822=ADVANCED_FACE ( 'NONE', ( #12029 ), #4791, .F. ) ;
#3826=EDGE_CURVE ( 'NONE', #11926, #3897, #3596, .T. ) ;
#3829=ORIENTED_EDGE ( 'NONE', *, *, #8105, .T. ) ;
#3836=LINE ( 'NONE', #10876, #18177 ) ;
#3839=ADVANCED_FACE ( 'NONE', ( #12130 ), #827, .T. ) ;
#3857=DIRECTION ( 'NONE',  ( 1.000000000000000000, 0.000000000000000000, 0.000000000000000000 ) ) ;
#3869=ORIENTED_EDGE ( 'NONE', *, *, #18169, .F. ) ;
#3879=CARTESIAN_POINT ( 'NONE',  ( 4.225031457058369810E-16, 2.299999999999999822, 7.599999999999999645 ) ) ;
#3897=VERTEX_POINT ( 'NONE', #456 ) ;
#3898=ORIENTED_EDGE ( 'NONE', *, *, #6448, .F. ) ;
#3911=EDGE_LOOP ( 'NONE', ( #6196, #3598, #13942, #13403 ) ) ;
#3917=VERTEX_POINT ( 'NONE', #11756 ) ;
#3922=ADVANCED_FACE ( 'NONE', ( #9332 ), #12489, .F. ) ;
#3928=LINE ( 'NONE', #6896, #14418 ) ;
#3930=CARTESIAN_POINT ( 'NONE',  ( 1.149999999999999911, 6.472933199251450276, 6.846017351831609865 ) ) ;
#3931=DIRECTION ( 'NONE',  ( 1.000000000000000000, 0.000000000000000000, 0.000000000000000000 ) ) ;
#3934=CARTESIAN_POINT ( 'NONE',  ( 1.800000000000000044, 11.40000000000000036, 6.599999999999999645 ) ) ;
#3945=ADVANCED_FACE ( 'NONE', ( #16739 ), #6749, .T. ) ;
#3959=DIRECTION ( 'NONE',  ( -1.000000000000000000, 0.000000000000000000, 0.000000000000000000 ) ) ;
#3966=EDGE_CURVE ( 'NONE', #15121, #15079, #12218, .T. ) ;
#3979=ORIENTED_EDGE ( 'NONE', *, *, #4492, .F. ) ;
#3985=VERTEX_POINT ( 'NONE', #15105 ) ;
#3989=CARTESIAN_POINT ( 'NONE',  ( -0.5999999999999999778, 11.40000000000000036, 7.700000000000000178 ) ) ;
#3990=DIRECTION ( 'NONE',  ( 1.000000000000000000, 0.000000000000000000, 0.000000000000000000 ) ) ;
#3995=EDGE_LOOP ( 'NONE', ( #12271, #17307, #13480, #15399 ) ) ;
#4025=ORIENTED_EDGE ( 'NONE', *, *, #6195, .T. ) ;
#4060=CARTESIAN_POINT ( 'NONE',  ( 1.899999999999999911, 11.40000000000000036, 6.599999999999999645 ) ) ;
#4086=LINE ( 'NONE', #15680, #13206 ) ;
#4087=DIRECTION ( 'NONE',  ( 1.000000000000000000, -2.220446049250309876E-16, -1.048990684667790150E-15 ) ) ;
#4093=ORIENTED_EDGE ( 'NONE', *, *, #8846, .F. ) ;
#4146=DIRECTION ( 'NONE',  ( 1.000000000000000000, 0.000000000000000000, 0.000000000000000000 ) ) ;
#4148=EDGE_LOOP ( 'NONE', ( #16986, #7271, #3617, #2123, #11243, #15003, #12400, #6485 ) ) ;
#4175=DIRECTION ( 'NONE',  ( 0.000000000000000000, -1.000000000000000000, 0.000000000000000000 ) ) ;
#4194=EDGE_CURVE ( 'NONE', #1195, #14289, #17373, .T. ) ;
#4201=FACE_OUTER_BOUND ( 'NONE', #8507, .T. ) ;
#4231=ORIENTED_EDGE ( 'NONE', *, *, #11624, .F. ) ;
#4233=PLANE ( 'NONE',  #2992 ) ;
#4258=DIRECTION ( 'NONE',  ( -1.000000000000000000, 2.220446049250309876E-16, -8.269460797427580527E-16 ) ) ;
#4262=LINE ( 'NONE', #15582, #15919 ) ;
#4273=EDGE_CURVE ( 'NONE', #1993, #2692, #10107, .T. ) ;
#4287=CARTESIAN_POINT ( 'NONE',  ( -1.149999999999999911, 9.299999999999998934, 7.500000000000000000 ) ) ;
#4288=CARTESIAN_POINT ( 'NONE',  ( 1.899999999999999911, 0.5999999999999999778, 6.599999999999999645 ) ) ;
#4317=CARTESIAN_POINT ( 'NONE',  ( -1.149999999999999911, 6.472933199251450276, 6.846017351831609865 ) ) ;
#4318=DIRECTION ( 'NONE',  ( -1.000000000000000000, 0.000000000000000000, 0.000000000000000000 ) ) ;
#4332=LINE ( 'NONE', #13890, #800 ) ;
#4334=CARTESIAN_POINT ( 'NONE',  ( -0.5999999999999999778, 10.80000000000000071, 7.599999999999999645 ) ) ;
#4341=VERTEX_POINT ( 'NONE', #195 ) ;
#4354=VECTOR ( 'NONE', #11735, 1000.000000000000000 ) ;
#4355=DIRECTION ( 'NONE',  ( 0.000000000000000000, 0.000000000000000000, -1.000000000000000000 ) ) ;
#4358=DIRECTION ( 'NONE',  ( -1.000000000000000000, 0.000000000000000000, 0.000000000000000000 ) ) ;
#4380=EDGE_CURVE ( 'NONE', #6428, #13183, #14622, .T. ) ;
#4403=VERTEX_POINT ( 'NONE', #10276 ) ;
#4407=EDGE_CURVE ( 'NONE', #2448, #7602, #4896, .T. ) ;
#4412=EDGE_LOOP ( 'NONE', ( #8223, #8414, #8474, #9171 ) ) ;
#4440=EDGE_LOOP ( 'NONE', ( #11659, #5141, #5944, #3237 ) ) ;
#4443=VERTEX_POINT ( 'NONE', #10832 ) ;
#4463=ORIENTED_EDGE ( 'NONE', *, *, #4380, .T. ) ;
#4492=EDGE_CURVE ( 'NONE', #7436, #15079, #10828, .T. ) ;
#4493=CARTESIAN_POINT ( 'NONE',  ( -1.149999999999999911, 9.274118095489749081, 7.596592582628910684 ) ) ;
#4508=PLANE ( 'NONE',  #2605 ) ;
#4509=LINE ( 'NONE', #4588, #4354 ) ;
#4549=DIRECTION ( 'NONE',  ( 1.000000000000000000, 0.000000000000000000, 0.000000000000000000 ) ) ;
#4571=CARTESIAN_POINT ( 'NONE',  ( -1.899999999999999911, 11.40000000000000036, 7.550000000000000711 ) ) ;
#4578=ORIENTED_EDGE ( 'NONE', *, *, #7807, .T. ) ;
#4579=LINE ( 'NONE', #17263, #16885 ) ;
#4587=DIRECTION ( 'NONE',  ( 1.000000000000000000, 0.000000000000000000, 0.000000000000000000 ) ) ;
#4588=CARTESIAN_POINT ( 'NONE',  ( 1.750000000000000000, 11.40000000000000036, 7.700000000000000178 ) ) ;
#4594=FACE_OUTER_BOUND ( 'NONE', #10753, .T. ) ;
#4598=DIRECTION ( 'NONE',  ( 0.000000000000000000, 0.000000000000000000, 1.000000000000000000 ) ) ;
#4624=VECTOR ( 'NONE', #7851, 1000.000000000000000 ) ;
#4669=AXIS2_PLACEMENT_3D ( 'NONE', #16543, #13753, #6249 ) ;
#4676=FACE_OUTER_BOUND ( 'NONE', #7393, .T. ) ;
#4682=DIRECTION ( 'NONE',  ( 1.224646799147350002E-16, -0.9659258262890690894, -0.2588190451025180749 ) ) ;
#4685=ORIENTED_EDGE ( 'NONE', *, *, #5316, .T. ) ;
#4719=LINE ( 'NONE', #16303, #15627 ) ;
#4727=VERTEX_POINT ( 'NONE', #9812 ) ;
#4729=EDGE_CURVE ( 'NONE', #9457, #16402, #16747, .T. ) ;
#4730=VERTEX_POINT ( 'NONE', #4060 ) ;
#4772=LINE ( 'NONE', #3381, #5354 ) ;
#4785=CARTESIAN_POINT ( 'NONE',  ( 1.699999999999999956, 2.299999999999999822, 7.599999999999999645 ) ) ;
#4786=DIRECTION ( 'NONE',  ( -1.000000000000000000, 2.381191005321109844E-32, 0.000000000000000000 ) ) ;
#4789=LINE ( 'NONE', #10640, #6032 ) ;
#4791=CYLINDRICAL_SURFACE ( 'NONE', #17330, 0.2750000000000000222 ) ;
#4813=ORIENTED_EDGE ( 'NONE', *, *, #16166, .F. ) ;
#4817=LINE ( 'NONE', #14558, #9385 ) ;
#4822=LINE ( 'NONE', #14742, #7334 ) ;
#4824=EDGE_CURVE ( 'NONE', #1993, #1835, #10490, .T. ) ;
#4827=ORIENTED_EDGE ( 'NONE', *, *, #8684, .T. ) ;
#4841=ORIENTED_EDGE ( 'NONE', *, *, #9045, .F. ) ;
#4845=DIRECTION ( 'NONE',  ( 0.000000000000000000, 0.000000000000000000, 1.000000000000000000 ) ) ;
#4862=CARTESIAN_POINT ( 'NONE',  ( -1.149999999999999911, 6.447051294741199534, 6.942609934460510779 ) ) ;
#4885=CARTESIAN_POINT ( 'NONE',  ( 0.5999999999999999778, 11.40000000000000036, 7.700000000000000178 ) ) ;
#4894=CIRCLE ( 'NONE', #16435, 0.2750000000000000222 ) ;
#4896=CIRCLE ( 'NONE', #5513, 0.1999999999999996503 ) ;
#4902=VERTEX_POINT ( 'NONE', #10406 ) ;
#4927=VECTOR ( 'NONE', #3346, 1000.000000000000000 ) ;
#4929=ADVANCED_FACE ( 'NONE', ( #16066 ), #13111, .F. ) ;
#4951=PLANE ( 'NONE',  #4669 ) ;
#4961=ADVANCED_FACE ( 'NONE', ( #15062 ), #14954, .T. ) ;
#4969=DIRECTION ( 'NONE',  ( 0.000000000000000000, 0.000000000000000000, -1.000000000000000000 ) ) ;
#4982=CARTESIAN_POINT ( 'NONE',  ( 1.149999999999999911, 9.299999999999998934, 7.599999999999999645 ) ) ;
#4993=VERTEX_POINT ( 'NONE', #12177 ) ;
#5006=ORIENTED_EDGE ( 'NONE', *, *, #3031, .T. ) ;
#5013=EDGE_CURVE ( 'NONE', #11655, #1195, #6707, .T. ) ;
#5018=LINE ( 'NONE', #8087, #12025 ) ;
#5048=EDGE_CURVE ( 'NONE', #15121, #747, #6143, .T. ) ;
#5049=ORIENTED_EDGE ( 'NONE', *, *, #14959, .F. ) ;
#5052=DIRECTION ( 'NONE',  ( 0.000000000000000000, 0.000000000000000000, 1.000000000000000000 ) ) ;
#5082=DIRECTION ( 'NONE',  ( 1.000000000000000000, -3.700743415417190112E-16, 0.000000000000000000 ) ) ;
#5098=CARTESIAN_POINT ( 'NONE',  ( -1.699999999999999956, 2.299999999999999822, 7.700000000000000178 ) ) ;
#5103=CARTESIAN_POINT ( 'NONE',  ( 1.750000000000000000, 11.40000000000000036, 7.550000000000000711 ) ) ;
#5141=ORIENTED_EDGE ( 'NONE', *, *, #760, .F. ) ;
#5149=FACE_OUTER_BOUND ( 'NONE', #16926, .T. ) ;
#5168=EDGE_CURVE ( 'NONE', #4341, #4730, #6982, .T. ) ;
#5174=EDGE_CURVE ( 'NONE', #4443, #14407, #9539, .T. ) ;
#5180=EDGE_CURVE ( 'NONE', #5374, #12675, #7359, .T. ) ;
#5185=VECTOR ( 'NONE', #13283, 1000.000000000000000 ) ;
#5190=EDGE_LOOP ( 'NONE', ( #11215, #17233, #12358, #17522 ) ) ;
#5223=DIRECTION ( 'NONE',  ( 1.445602896647339508E-15, 0.000000000000000000, 1.000000000000000000 ) ) ;
#5232=VECTOR ( 'NONE', #17268, 1000.000000000000000 ) ;
#5233=CARTESIAN_POINT ( 'NONE',  ( 0.5999999999999999778, 10.80000000000000071, 7.700000000000000178 ) ) ;
#5237=FACE_BOUND ( 'NONE', #12867, .T. ) ;
#5248=VECTOR ( 'NONE', #12457, 1000.000000000000000 ) ;
#5255=AXIS2_PLACEMENT_3D ( 'NONE', #11225, #4087, #16869 ) ;
#5257=VECTOR ( 'NONE', #12708, 1000.000000000000000 ) ;
#5293=DIRECTION ( 'NONE',  ( 0.7071067811865480168, 0.7071067811865470176, 0.000000000000000000 ) ) ;
#5295=VERTEX_POINT ( 'NONE', #16893 ) ;
#5298=EDGE_CURVE ( 'NONE', #9985, #2611, #15518, .T. ) ;
#5316=EDGE_CURVE ( 'NONE', #1663, #4341, #4822, .T. ) ;
#5335=CARTESIAN_POINT ( 'NONE',  ( 0.9499999999999999556, 2.299999999999999822, 7.599999999999999645 ) ) ;
#5338=LINE ( 'NONE', #10984, #2322 ) ;
#5342=LINE ( 'NONE', #3934, #5927 ) ;
#5354=VECTOR ( 'NONE', #14677, 1000.000000000000000 ) ;
#5356=CARTESIAN_POINT ( 'NONE',  ( 1.699999999999999956, 9.299999999999998934, 7.700000000000000178 ) ) ;
#5367=PRODUCT ( 'Top Metal Cover Plate', 'Top Metal Cover Plate', '', ( #14834 ) ) ;
#5372=DIRECTION ( 'NONE',  ( 1.000000000000000000, -1.850371707708589879E-16, 0.000000000000000000 ) ) ;
#5374=VERTEX_POINT ( 'NONE', #11600 ) ;
#5402=LINE ( 'NONE', #9653, #11307 ) ;
#5412=AXIS2_PLACEMENT_3D ( 'NONE', #9008, #14660, #4845 ) ;
#5418=CARTESIAN_POINT ( 'NONE',  ( 1.699999999999999956, 9.299999999999998934, 7.599999999999999645 ) ) ;
#5419=EDGE_CURVE ( 'NONE', #5295, #8002, #16792, .T. ) ;
#5442=LINE ( 'NONE', #7118, #8195 ) ;
#5453=CARTESIAN_POINT ( 'NONE',  ( -1.149999999999999911, 9.299999999999998934, 7.599999999999999645 ) ) ;
#5459=CARTESIAN_POINT ( 'NONE',  ( 1.149999999999999911, 9.299999999999998934, 7.700000000000000178 ) ) ;
#5463=DIRECTION ( 'NONE',  ( 0.000000000000000000, 0.000000000000000000, 1.000000000000000000 ) ) ;
#5467=CARTESIAN_POINT ( 'NONE',  ( -1.899999999999999911, 0.5999999999999999778, 7.700000000000000178 ) ) ;
#5481=CARTESIAN_POINT ( 'NONE',  ( 3.371799150351489833E-16, 2.299999999999999822, 7.599999999999999645 ) ) ;
#5494=VECTOR ( 'NONE', #3990, 1000.000000000000000 ) ;
#5513=AXIS2_PLACEMENT_3D ( 'NONE', #15945, #3245, #8889 ) ;
#5526=AXIS2_PLACEMENT_3D ( 'NONE', #12999, #1877, #230 ) ;
#5550=CIRCLE ( 'NONE', #7035, 0.1000000000000003247 ) ;
#5563=ORIENTED_EDGE ( 'NONE', *, *, #86, .T. ) ;
#5567=EDGE_CURVE ( 'NONE', #7602, #7108, #12717, .T. ) ;
#5568=EDGE_LOOP ( 'NONE', ( #901, #9935, #11326, #7967 ) ) ;
#5576=PLANE ( 'NONE',  #2898 ) ;
#5581=PLANE ( 'NONE',  #5255 ) ;
#5613=PLANE ( 'NONE',  #303 ) ;
#5621=AXIS2_PLACEMENT_3D ( 'NONE', #8499, #12484, #1281 ) ;
#5635=DIRECTION ( 'NONE',  ( 0.000000000000000000, 0.000000000000000000, 1.000000000000000000 ) ) ;
#5654=DIRECTION ( 'NONE',  ( -1.000000000000000000, -1.776356839400250070E-15, 0.000000000000000000 ) ) ;
#5658=AXIS2_PLACEMENT_3D ( 'NONE', #11830, #8769, #13125 ) ;
#5667=ORIENTED_EDGE ( 'NONE', *, *, #3511, .F. ) ;
#5671=CARTESIAN_POINT ( 'NONE',  ( 0.9499999999999999556, 2.299999999999999822, 7.599999999999999645 ) ) ;
#5679=DIRECTION ( 'NONE',  ( 7.656710514656250048E-17, -0.9659258262890690894, -0.2588190451025180749 ) ) ;
#5692=EDGE_CURVE ( 'NONE', #16402, #12675, #12806, .T. ) ;
#5703=CARTESIAN_POINT ( 'NONE',  ( 1.699999999999999956, 9.299999999999998934, 7.599999999999999645 ) ) ;
#5712=VERTEX_POINT ( 'NONE', #10027 ) ;
#5723=DIRECTION ( 'NONE',  ( 0.000000000000000000, 0.000000000000000000, 1.000000000000000000 ) ) ;
#5729=DIRECTION ( 'NONE',  ( 0.000000000000000000, 0.000000000000000000, 1.000000000000000000 ) ) ;
#5745=VERTEX_POINT ( 'NONE', #7248 ) ;
#5747=CARTESIAN_POINT ( 'NONE',  ( 1.750000000000000000, 11.40000000000000036, 7.599999999999999645 ) ) ;
#5756=CARTESIAN_POINT ( 'NONE',  ( 0.2750000000000004663, 2.299999999999999822, 7.599999999999999645 ) ) ;
#5765=DIRECTION ( 'NONE',  ( 0.000000000000000000, 0.000000000000000000, 1.000000000000000000 ) ) ;
#5783=CARTESIAN_POINT ( 'NONE',  ( -1.750000000000000000, 11.40000000000000036, 7.550000000000000711 ) ) ;
#5814=AXIS2_PLACEMENT_3D ( 'NONE', #18256, #9577, #13841 ) ;
#5828=EDGE_LOOP ( 'NONE', ( #10663, #906, #17385, #17329 ) ) ;
#5847=VECTOR ( 'NONE', #15866, 1000.000000000000000 ) ;
#5872=CARTESIAN_POINT ( 'NONE',  ( -0.5999999999999999778, 11.40000000000000036, 7.599999999999999645 ) ) ;
#5876=EDGE_CURVE ( 'NONE', #1173, #3985, #3696, .T. ) ;
#5878=EDGE_CURVE ( 'NONE', #3985, #5295, #7594, .T. ) ;
#5902=EDGE_CURVE ( 'NONE', #2720, #4993, #4719, .T. ) ;
#5914=CARTESIAN_POINT ( 'NONE',  ( -1.800000000000000044, 0.5999999999999999778, 6.599999999999999645 ) ) ;
#5927=VECTOR ( 'NONE', #15248, 1000.000000000000000 ) ;
#5944=ORIENTED_EDGE ( 'NONE', *, *, #1495, .T. ) ;
#5969=ADVANCED_FACE ( 'NONE', ( #6576 ), #6941, .T. ) ;
#5976=EDGE_CURVE ( 'NONE', #3272, #13978, #1297, .T. ) ;
#6011=ORIENTED_EDGE ( 'NONE', *, *, #324, .T. ) ;
#6020=( LENGTH_UNIT ( ) NAMED_UNIT ( * ) SI_UNIT ( .MILLI., .METRE. ) );
#6022=DIRECTION ( 'NONE',  ( 0.000000000000000000, 0.000000000000000000, 1.000000000000000000 ) ) ;
#6032=VECTOR ( 'NONE', #14901, 1000.000000000000000 ) ;
#6043=VERTEX_POINT ( 'NONE', #5467 ) ;
#6049=VERTEX_POINT ( 'NONE', #3801 ) ;
#6056=ORIENTED_EDGE ( 'NONE', *, *, #754, .T. ) ;
#6058=CARTESIAN_POINT ( 'NONE',  ( -1.300000000000000044, 1.592040838891560081E-16, 7.599999999999999645 ) ) ;
#6083=DIRECTION ( 'NONE',  ( 0.000000000000000000, 0.000000000000000000, -1.000000000000000000 ) ) ;
#6104=VECTOR ( 'NONE', #17124, 1000.000000000000000 ) ;
#6121=FACE_OUTER_BOUND ( 'NONE', #10866, .T. ) ;
#6130=AXIS2_PLACEMENT_3D ( 'NONE', #14736, #8910, #17315 ) ;
#6137=EDGE_CURVE ( 'NONE', #7174, #2720, #1760, .T. ) ;
#6143=CIRCLE ( 'NONE', #17364, 0.1499999999999999667 ) ;
#6146=VECTOR ( 'NONE', #4598, 1000.000000000000000 ) ;
#6150=ORIENTED_EDGE ( 'NONE', *, *, #5168, .T. ) ;
#6159=DIRECTION ( 'NONE',  ( 2.055968564120659776E-16, 1.000000000000000000, 0.000000000000000000 ) ) ;
#6162=ORIENTED_EDGE ( 'NONE', *, *, #215, .T. ) ;
#6195=EDGE_CURVE ( 'NONE', #7698, #796, #17019, .T. ) ;
#6196=ORIENTED_EDGE ( 'NONE', *, *, #16146, .F. ) ;
#6249=DIRECTION ( 'NONE',  ( 1.000000000000000000, 0.000000000000000000, 0.000000000000000000 ) ) ;
#6250=CARTESIAN_POINT ( 'NONE',  ( 1.750000000000000000, 0.5999999999999999778, 7.599999999999999645 ) ) ;
#6253=ORIENTED_EDGE ( 'NONE', *, *, #6642, .F. ) ;
#6269=DIRECTION ( 'NONE',  ( 1.000000000000000000, -1.903239470785979823E-16, 0.000000000000000000 ) ) ;
#6290=EDGE_CURVE ( 'NONE', #12675, #4902, #10096, .T. ) ;
#6295=ADVANCED_FACE ( 'NONE', ( #14609 ), #14799, .F. ) ;
#6298=DIRECTION ( 'NONE',  ( 0.000000000000000000, 0.000000000000000000, 1.000000000000000000 ) ) ;
#6321=CARTESIAN_POINT ( 'NONE',  ( 1.750000000000000000, 0.5999999999999999778, 7.599999999999999645 ) ) ;
#6330=FACE_OUTER_BOUND ( 'NONE', #9462, .T. ) ;
#6375=VECTOR ( 'NONE', #7844, 1000.000000000000000 ) ;
#6382=ORIENTED_EDGE ( 'NONE', *, *, #10319, .T. ) ;
#6388=CYLINDRICAL_SURFACE ( 'NONE', #17631, 0.9499999999999999556 ) ;
#6391=CARTESIAN_POINT ( 'NONE',  ( -0.2749999999999995781, 2.299999999999999822, 7.599999999999999645 ) ) ;
#6428=VERTEX_POINT ( 'NONE', #7783 ) ;
#6429=FACE_OUTER_BOUND ( 'NONE', #748, .T. ) ;
#6433=ORIENTED_EDGE ( 'NONE', *, *, #6137, .F. ) ;
#6436=VECTOR ( 'NONE', #10501, 1000.000000000000000 ) ;
#6437=EDGE_LOOP ( 'NONE', ( #10207, #15695, #11755, #5049 ) ) ;
#6441=ORIENTED_EDGE ( 'NONE', *, *, #9347, .F. ) ;
#6443=VECTOR ( 'NONE', #10949, 1000.000000000000000 ) ;
#6448=EDGE_CURVE ( 'NONE', #5712, #1195, #1369, .T. ) ;
#6449=DIRECTION ( 'NONE',  ( 1.000000000000000000, 0.000000000000000000, 0.000000000000000000 ) ) ;
#6473=ADVANCED_FACE ( 'NONE', ( #10158 ), #7295, .T. ) ;
#6485=ORIENTED_EDGE ( 'NONE', *, *, #15636, .T. ) ;
#6487=DIRECTION ( 'NONE',  ( -1.000000000000000000, -1.850371707708589879E-16, 0.000000000000000000 ) ) ;
#6504=EDGE_CURVE ( 'NONE', #7625, #10238, #8679, .T. ) ;
#6550=DIRECTION ( 'NONE',  ( -8.269460797427580527E-16, 0.000000000000000000, 1.000000000000000000 ) ) ;
#6564=CARTESIAN_POINT ( 'NONE',  ( 0.5999999999999999778, 11.40000000000000036, 7.700000000000000178 ) ) ;
#6576=FACE_OUTER_BOUND ( 'NONE', #10211, .T. ) ;
#6612=CARTESIAN_POINT ( 'NONE',  ( 0.5999999999999999778, -7.347880794884110368E-17, 7.599999999999999645 ) ) ;
#6626=AXIS2_PLACEMENT_3D ( 'NONE', #11026, #6862, #943 ) ;
#6627=DIRECTION ( 'NONE',  ( 1.000000000000000000, 0.000000000000000000, 0.000000000000000000 ) ) ;
#6637=PLANE ( 'NONE',  #12619 ) ;
#6642=EDGE_CURVE ( 'NONE', #17362, #16159, #11637, .T. ) ;
#6707=LINE ( 'NONE', #16335, #13783 ) ;
#6749=PLANE ( 'NONE',  #15859 ) ;
#6763=AXIS2_PLACEMENT_3D ( 'NONE', #17609, #17235, #11803 ) ;
#6778=CARTESIAN_POINT ( 'NONE',  ( 1.699999999999999956, 2.299999999999999822, 7.599999999999999645 ) ) ;
#6793=CARTESIAN_POINT ( 'NONE',  ( 1.750000000000000000, 0.5999999999999999778, 7.599999999999999645 ) ) ;
#6803=VECTOR ( 'NONE', #2313, 1000.000000000000000 ) ;
#6833=CARTESIAN_POINT ( 'NONE',  ( -1.699999999999999956, 9.299999999999998934, 7.700000000000000178 ) ) ;
#6861=APPLICATION_CONTEXT ( 'automotive_design' ) ;
#6862=DIRECTION ( 'NONE',  ( 0.000000000000000000, 0.000000000000000000, -1.000000000000000000 ) ) ;
#6872=ADVANCED_FACE ( 'NONE', ( #5149 ), #13682, .F. ) ;
#6883=ORIENTED_EDGE ( 'NONE', *, *, #639, .F. ) ;
#6896=CARTESIAN_POINT ( 'NONE',  ( 1.800000000000000044, 0.5999999999999999778, 7.550000000000000711 ) ) ;
#6917=DIRECTION ( 'NONE',  ( 1.903239470785979823E-16, 1.000000000000000000, 0.000000000000000000 ) ) ;
#6926=ORIENTED_EDGE ( 'NONE', *, *, #187, .F. ) ;
#6929=DIRECTION ( 'NONE',  ( -2.220446049250309876E-16, -1.000000000000000000, 0.000000000000000000 ) ) ;
#6935=CARTESIAN_POINT ( 'NONE',  ( -0.5999999999999999778, 0.5999999999999999778, 7.599999999999999645 ) ) ;
#6939=LINE ( 'NONE', #12586, #2254 ) ;
#6941=PLANE ( 'NONE',  #9966 ) ;
#6942=ORIENTED_EDGE ( 'NONE', *, *, #3966, .T. ) ;
#6944=EDGE_LOOP ( 'NONE', ( #13956, #15810, #11262, #15555 ) ) ;
#6965=DIRECTION ( 'NONE',  ( 2.220446049250309876E-16, 1.000000000000000000, 1.841437368383549833E-16 ) ) ;
#6970=DIRECTION ( 'NONE',  ( 0.7071067811865480168, 0.7071067811865470176, 0.000000000000000000 ) ) ;
#6982=LINE ( 'NONE', #4288, #14550 ) ;
#7019=CARTESIAN_POINT ( 'NONE',  ( 1.699999999999999956, 2.299999999999999822, 7.700000000000000178 ) ) ;
#7026=EDGE_LOOP ( 'NONE', ( #15601, #3384, #6441, #10897 ) ) ;
#7028=VECTOR ( 'NONE', #15557, 1000.000000000000000 ) ;
#7032=CARTESIAN_POINT ( 'NONE',  ( -1.899999999999999911, 0.5999999999999999778, 6.599999999999999645 ) ) ;
#7035=AXIS2_PLACEMENT_3D ( 'NONE', #2524, #13816, #1228 ) ;
#7044=AXIS2_PLACEMENT_3D ( 'NONE', #7101, #13939, #3931 ) ;
#7053=EDGE_LOOP ( 'NONE', ( #12017, #10171, #11903, #14598 ) ) ;
#7069=VECTOR ( 'NONE', #8969, 1000.000000000000000 ) ;
#7101=CARTESIAN_POINT ( 'NONE',  ( 1.699999999999999956, 9.299999999999998934, 7.599999999999999645 ) ) ;
#7104=EDGE_CURVE ( 'NONE', #8925, #4902, #1352, .T. ) ;
#7108=VERTEX_POINT ( 'NONE', #14132 ) ;
#7110=AXIS2_PLACEMENT_3D ( 'NONE', #15926, #17194, #17467 ) ;
#7118=CARTESIAN_POINT ( 'NONE',  ( -1.699999999999999956, 2.299999999999999822, 7.599999999999999645 ) ) ;
#7122=PRODUCT_DEFINITION ( 'UNKNOWN', '', #1478, #1396 ) ;
#7136=ORIENTED_EDGE ( 'NONE', *, *, #34, .T. ) ;
#7150=VERTEX_POINT ( 'NONE', #16909 ) ;
#7174=VERTEX_POINT ( 'NONE', #17077 ) ;
#7204=LINE ( 'NONE', #12846, #14573 ) ;
#7228=PLANE ( 'NONE',  #10757 ) ;
#7248=CARTESIAN_POINT ( 'NONE',  ( -0.2749999999999995781, 2.299999999999999822, 7.700000000000000178 ) ) ;
#7253=ORIENTED_EDGE ( 'NONE', *, *, #15815, .T. ) ;
#7255=ORIENTED_EDGE ( 'NONE', *, *, #8066, .T. ) ;
#7263=DIRECTION ( 'NONE',  ( 1.000000000000000000, 0.000000000000000000, 0.000000000000000000 ) ) ;
#7271=ORIENTED_EDGE ( 'NONE', *, *, #108, .T. ) ;
#7284=EDGE_CURVE ( 'NONE', #4993, #3917, #811, .T. ) ;
#7295=PLANE ( 'NONE',  #18248 ) ;
#7296=VECTOR ( 'NONE', #12244, 1000.000000000000000 ) ;
#7311=AXIS2_PLACEMENT_3D ( 'NONE', #5671, #4175, #12881 ) ;
#7327=VECTOR ( 'NONE', #8686, 1000.000000000000000 ) ;
#7334=VECTOR ( 'NONE', #3531, 1000.000000000000000 ) ;
#7359=LINE ( 'NONE', #15782, #9694 ) ;
#7361=LINE ( 'NONE', #408, #11167 ) ;
#7368=EDGE_CURVE ( 'NONE', #8925, #17576, #10385, .T. ) ;
#7378=VECTOR ( 'NONE', #7955, 1000.000000000000114 ) ;
#7392=ORIENTED_EDGE ( 'NONE', *, *, #5168, .F. ) ;
#7393=EDGE_LOOP ( 'NONE', ( #17224, #12768, #2511, #1301 ) ) ;
#7396=ORIENTED_EDGE ( 'NONE', *, *, #5013, .T. ) ;
#7397=FACE_OUTER_BOUND ( 'NONE', #14676, .T. ) ;
#7433=ORIENTED_EDGE ( 'NONE', *, *, #16055, .F. ) ;
#7436=VERTEX_POINT ( 'NONE', #17574 ) ;
#7449=EDGE_CURVE ( 'NONE', #3897, #4403, #4817, .T. ) ;
#7483=AXIS2_PLACEMENT_3D ( 'NONE', #11368, #15547, #1559 ) ;
#7492=ORIENTED_EDGE ( 'NONE', *, *, #12897, .F. ) ;
#7580=DIRECTION ( 'NONE',  ( -1.000000000000000000, 0.000000000000000000, 0.000000000000000000 ) ) ;
#7582=ORIENTED_EDGE ( 'NONE', *, *, #14353, .F. ) ;
#7585=SURFACE_SIDE_STYLE ('',( #8974 ) ) ;
#7587=VECTOR ( 'NONE', #6917, 1000.000000000000000 ) ;
#7594=LINE ( 'NONE', #13245, #2300 ) ;
#7602=VERTEX_POINT ( 'NONE', #193 ) ;
#7625=VERTEX_POINT ( 'NONE', #16950 ) ;
#7640=CARTESIAN_POINT ( 'NONE',  ( -1.899999999999999911, 11.40000000000000036, 7.550000000000000711 ) ) ;
#7648=LINE ( 'NONE', #13198, #15163 ) ;
#7655=AXIS2_PLACEMENT_3D ( 'NONE', #9520, #15178, #2487 ) ;
#7664=ADVANCED_FACE ( 'NONE', ( #11119 ), #5576, .T. ) ;
#7682=EDGE_CURVE ( 'NONE', #14961, #8260, #16766, .T. ) ;
#7692=CARTESIAN_POINT ( 'NONE',  ( 1.899999999999999911, 11.40000000000000036, 7.599999999999999645 ) ) ;
#7698=VERTEX_POINT ( 'NONE', #5756 ) ;
#7783=CARTESIAN_POINT ( 'NONE',  ( 1.699999999999999956, 2.299999999999999822, 7.599999999999999645 ) ) ;
#7784=LINE ( 'NONE', #1033, #14618 ) ;
#7797=LINE ( 'NONE', #17776, #7296 ) ;
#7807=EDGE_CURVE ( 'NONE', #8002, #16159, #16108, .T. ) ;
#7844=DIRECTION ( 'NONE',  ( -3.700743415417179758E-16, -1.000000000000000000, 0.000000000000000000 ) ) ;
#7851=DIRECTION ( 'NONE',  ( -9.349246523159200620E-16, 0.000000000000000000, 1.000000000000000000 ) ) ;
#7856=ORIENTED_EDGE ( 'NONE', *, *, #13908, .F. ) ;
#7881=EDGE_LOOP ( 'NONE', ( #7582, #11503, #7255, #2389 ) ) ;
#7898=ORIENTED_EDGE ( 'NONE', *, *, #2452, .T. ) ;
#7910=VECTOR ( 'NONE', #10655, 1000.000000000000114 ) ;
#7913=DIRECTION ( 'NONE',  ( 0.000000000000000000, 0.000000000000000000, 1.000000000000000000 ) ) ;
#7950=CARTESIAN_POINT ( 'NONE',  ( 0.5999999999999999778, 11.40000000000000036, 7.599999999999999645 ) ) ;
#7955=DIRECTION ( 'NONE',  ( 0.000000000000000000, -0.2588190451025180749, 0.9659258262890690894 ) ) ;
#7967=ORIENTED_EDGE ( 'NONE', *, *, #16143, .T. ) ;
#7977=DIRECTION ( 'NONE',  ( -1.000000000000000000, 1.903239470785979823E-16, 0.000000000000000000 ) ) ;
#7980=DIRECTION ( 'NONE',  ( -1.000000000000000000, 0.000000000000000000, 0.000000000000000000 ) ) ;
#7982=ORIENTED_EDGE ( 'NONE', *, *, #187, .T. ) ;
#7987=EDGE_LOOP ( 'NONE', ( #14576, #15668, #4093, #11981 ) ) ;
#7996=ORIENTED_EDGE ( 'NONE', *, *, #17471, .F. ) ;
#8002=VERTEX_POINT ( 'NONE', #5459 ) ;
#8005=ORIENTED_EDGE ( 'NONE', *, *, #13471, .T. ) ;
#8019=DIRECTION ( 'NONE',  ( 1.000000000000000000, -2.220446049250309876E-16, 0.000000000000000000 ) ) ;
#8023=DIRECTION ( 'NONE',  ( -1.000000000000000000, 0.000000000000000000, 0.000000000000000000 ) ) ;
#8027=VECTOR ( 'NONE', #12154, 1000.000000000000000 ) ;
#8039=FACE_OUTER_BOUND ( 'NONE', #9119, .T. ) ;
#8048=CARTESIAN_POINT ( 'NONE',  ( -1.800000000000000044, 11.40000000000000036, 7.550000000000000711 ) ) ;
#8058=LINE ( 'NONE', #4982, #6803 ) ;
#8061=DIRECTION ( 'NONE',  ( -3.700743415417179758E-16, -1.000000000000000000, 0.000000000000000000 ) ) ;
#8065=CARTESIAN_POINT ( 'NONE',  ( -1.149999999999999911, 9.274118095489749081, 7.596592582628910684 ) ) ;
#8066=EDGE_CURVE ( 'NONE', #14289, #2611, #11554, .T. ) ;
#8078=CARTESIAN_POINT ( 'NONE',  ( 1.300000000000000044, -1.592040838891560081E-16, 7.599999999999999645 ) ) ;
#8081=ORIENTED_EDGE ( 'NONE', *, *, #17766, .T. ) ;
#8083=ADVANCED_FACE ( 'NONE', ( #17186 ), #4508, .T. ) ;
#8085=LINE ( 'NONE', #6778, #15720 ) ;
#8087=CARTESIAN_POINT ( 'NONE',  ( -1.149999999999999911, 9.299999999999998934, 7.700000000000000178 ) ) ;
#8105=EDGE_CURVE ( 'NONE', #14407, #7625, #533, .T. ) ;
#8108=AXIS2_PLACEMENT_3D ( 'NONE', #1126, #6487, #942 ) ;
#8110=DIRECTION ( 'NONE',  ( 1.000000000000000000, 5.551115123125880521E-15, -8.881784197001400629E-15 ) ) ;
#8165=ORIENTED_EDGE ( 'NONE', *, *, #14460, .F. ) ;
#8179=EDGE_LOOP ( 'NONE', ( #11449, #1448, #522, #12872 ) ) ;
#8195=VECTOR ( 'NONE', #16996, 1000.000000000000000 ) ;
#8208=DIRECTION ( 'NONE',  ( -6.162975822039146519E-33, -0.2588190451025180749, 0.9659258262890690894 ) ) ;
#8220=AXIS2_PLACEMENT_3D ( 'NONE', #14893, #14795, #2108 ) ;
#8223=ORIENTED_EDGE ( 'NONE', *, *, #18172, .T. ) ;
#8228=LINE ( 'NONE', #17923, #9228 ) ;
#8245=EDGE_CURVE ( 'NONE', #2916, #4730, #16271, .T. ) ;
#8254=DIRECTION ( 'NONE',  ( -1.048990684667790150E-15, 0.000000000000000000, -1.000000000000000000 ) ) ;
#8256=EDGE_LOOP ( 'NONE', ( #850, #1082, #14805, #14570 ) ) ;
#8260=VERTEX_POINT ( 'NONE', #16177 ) ;
#8272=CARTESIAN_POINT ( 'NONE',  ( -1.899999999999999911, 0.5999999999999999778, 7.550000000000000711 ) ) ;
#8294=CARTESIAN_POINT ( 'NONE',  ( 1.750000000000060174, 0.5999999999999999778, 7.550000000000000711 ) ) ;
#8298=LINE ( 'NONE', #5335, #5248 ) ;
#8329=LINE ( 'NONE', #6564, #14923 ) ;
#8332=CARTESIAN_POINT ( 'NONE',  ( -1.699999999999999956, 2.299999999999999822, 7.599999999999999645 ) ) ;
#8341=CARTESIAN_POINT ( 'NONE',  ( 1.899999999999999911, 0.5999999999999999778, 7.550000000000000711 ) ) ;
#8357=DIRECTION ( 'NONE',  ( -1.000000000000000000, 0.000000000000000000, 0.000000000000000000 ) ) ;
#8370=EDGE_CURVE ( 'NONE', #15079, #8647, #12917, .T. ) ;
#8383=DIRECTION ( 'NONE',  ( 0.000000000000000000, 0.000000000000000000, 1.000000000000000000 ) ) ;
#8405=LINE ( 'NONE', #12664, #18221 ) ;
#8408=LINE ( 'NONE', #7019, #12384 ) ;
#8414=ORIENTED_EDGE ( 'NONE', *, *, #9286, .T. ) ;
#8430=FACE_OUTER_BOUND ( 'NONE', #1050, .T. ) ;
#8443=LINE ( 'NONE', #14190, #5494 ) ;
#8445=EDGE_CURVE ( 'NONE', #16779, #616, #17282, .T. ) ;
#8463=AXIS2_PLACEMENT_3D ( 'NONE', #10538, #3603, #9252 ) ;
#8469=DIRECTION ( 'NONE',  ( -2.220446049250309876E-16, -1.000000000000000000, 4.958742624062499518E-17 ) ) ;
#8474=ORIENTED_EDGE ( 'NONE', *, *, #5878, .F. ) ;
#8499=CARTESIAN_POINT ( 'NONE',  ( 4.225031457058369810E-16, 2.299999999999999822, 7.599999999999999645 ) ) ;
#8507=EDGE_LOOP ( 'NONE', ( #14502, #4685, #11623, #14880 ) ) ;
#8597=ORIENTED_EDGE ( 'NONE', *, *, #14365, .T. ) ;
#8603=EDGE_LOOP ( 'NONE', ( #11131, #7253, #12104, #597 ) ) ;
#8610=CARTESIAN_POINT ( 'NONE',  ( 1.750000000000000000, 11.40000000000000036, 7.599999999999999645 ) ) ;
#8614=LINE ( 'NONE', #4334, #12902 ) ;
#8621=ORIENTED_EDGE ( 'NONE', *, *, #14460, .T. ) ;
#8647=VERTEX_POINT ( 'NONE', #4885 ) ;
#8656=ORIENTED_EDGE ( 'NONE', *, *, #5692, .F. ) ;
#8679=LINE ( 'NONE', #18191, #12663 ) ;
#8684=EDGE_CURVE ( 'NONE', #5295, #7602, #3400, .T. ) ;
#8686=DIRECTION ( 'NONE',  ( 1.000000000000000000, 0.000000000000000000, 0.000000000000000000 ) ) ;
#8694=DIRECTION ( 'NONE',  ( 0.000000000000000000, -1.000000000000000000, 0.000000000000000000 ) ) ;
#8704=ORIENTED_EDGE ( 'NONE', *, *, #6448, .T. ) ;
#8733=EDGE_CURVE ( 'NONE', #14961, #16021, #17650, .T. ) ;
#8768=EDGE_LOOP ( 'NONE', ( #16063, #4231, #790, #17871 ) ) ;
#8769=DIRECTION ( 'NONE',  ( 2.220446049250309876E-16, 1.000000000000000000, -5.551115123125800057E-15 ) ) ;
#8770=DIRECTION ( 'NONE',  ( -9.349246523159200620E-16, 0.000000000000000000, 1.000000000000000000 ) ) ;
#8780=DIRECTION ( 'NONE',  ( -1.000000000000000000, 0.000000000000000000, 1.048990684667790150E-15 ) ) ;
#8798=ADVANCED_FACE ( 'NONE', ( #17753 ), #1017, .T. ) ;
#8846=EDGE_CURVE ( 'NONE', #4727, #5712, #10734, .T. ) ;
#8854=FACE_OUTER_BOUND ( 'NONE', #8768, .T. ) ;
#8889=DIRECTION ( 'NONE',  ( 0.000000000000000000, 0.000000000000000000, 1.000000000000000000 ) ) ;
#8897=EDGE_CURVE ( 'NONE', #13468, #1492, #13615, .T. ) ;
#8898=DIRECTION ( 'NONE',  ( -1.000000000000000000, 0.000000000000000000, 0.000000000000000000 ) ) ;
#8910=DIRECTION ( 'NONE',  ( -5.401922984254539957E-62, -1.000000000000000000, 1.836189155707839943E-31 ) ) ;
#8912=ORIENTED_EDGE ( 'NONE', *, *, #9347, .T. ) ;
#8920=ORIENTED_EDGE ( 'NONE', *, *, #11096, .F. ) ;
#8925=VERTEX_POINT ( 'NONE', #13965 ) ;
#8936=CARTESIAN_POINT ( 'NONE',  ( -1.800000000000000044, 0.5999999999999999778, 7.550000000000000711 ) ) ;
#8957=DIRECTION ( 'NONE',  ( -1.000000000000000000, 2.220446049250309876E-16, 0.000000000000000000 ) ) ;
#8969=DIRECTION ( 'NONE',  ( -1.000000000000000000, 0.000000000000000000, 0.000000000000000000 ) ) ;
#8974=SURFACE_STYLE_FILL_AREA ( #15943 ) ;
#8986=CARTESIAN_POINT ( 'NONE',  ( 1.149999999999999911, 6.472933199251450276, 6.846017351831609865 ) ) ;
#8993=ORIENTED_EDGE ( 'NONE', *, *, #8445, .T. ) ;
#9008=CARTESIAN_POINT ( 'NONE',  ( 1.750000000000000000, 0.5999999999999999778, 7.550000000000000711 ) ) ;
#9045=EDGE_CURVE ( 'NONE', #16779, #7436, #13401, .T. ) ;
#9047=DIRECTION ( 'NONE',  ( -3.700743415417190112E-16, -1.000000000000000000, 0.000000000000000000 ) ) ;
#9090=VECTOR ( 'NONE', #16584, 1000.000000000000000 ) ;
#9097=DIRECTION ( 'NONE',  ( 0.000000000000000000, 0.000000000000000000, 1.000000000000000000 ) ) ;
#9103=DIRECTION ( 'NONE',  ( -1.224646799147350002E-16, -1.000000000000000000, 0.000000000000000000 ) ) ;
#9119=EDGE_LOOP ( 'NONE', ( #14941, #11784, #15193, #9634 ) ) ;
#9122=CIRCLE ( 'NONE', #1162, 0.2750000000000000222 ) ;
#9147=DIRECTION ( 'NONE',  ( 0.000000000000000000, 0.000000000000000000, 1.000000000000000000 ) ) ;
#9171=ORIENTED_EDGE ( 'NONE', *, *, #5876, .F. ) ;
#9178=VERTEX_POINT ( 'NONE', #16367 ) ;
#9228=VECTOR ( 'NONE', #3959, 1000.000000000000000 ) ;
#9246=ORIENTED_EDGE ( 'NONE', *, *, #2452, .F. ) ;
#9252=DIRECTION ( 'NONE',  ( 1.000000000000000000, 0.000000000000000000, 0.000000000000000000 ) ) ;
#9262=DIRECTION ( 'NONE',  ( 0.000000000000000000, 0.000000000000000000, 1.000000000000000000 ) ) ;
#9286=EDGE_CURVE ( 'NONE', #10172, #5295, #12206, .T. ) ;
#9317=AXIS2_PLACEMENT_3D ( 'NONE', #14014, #17286, #9660 ) ;
#9323=DIRECTION ( 'NONE',  ( -6.162975822039146519E-33, -0.2588190451025180749, 0.9659258262890690894 ) ) ;
#9332=FACE_OUTER_BOUND ( 'NONE', #4440, .T. ) ;
#9333=CARTESIAN_POINT ( 'NONE',  ( -1.899999999999999911, 11.40000000000000036, 6.599999999999999645 ) ) ;
#9343=VECTOR ( 'NONE', #422, 1000.000000000000000 ) ;
#9347=EDGE_CURVE ( 'NONE', #8260, #12172, #10809, .T. ) ;
#9352=EDGE_CURVE ( 'NONE', #7150, #9659, #14453, .T. ) ;
#9359=CIRCLE ( 'NONE', #1382, 0.9499999999999999556 ) ;
#9362=AXIS2_PLACEMENT_3D ( 'NONE', #17751, #5082, #9047 ) ;
#9380=CARTESIAN_POINT ( 'NONE',  ( -1.149999999999999911, 9.299999999999998934, 7.599999999999999645 ) ) ;
#9382=CARTESIAN_POINT ( 'NONE',  ( 0.5999999999999999778, 0.5999999999999999778, 7.700000000000000178 ) ) ;
#9385=VECTOR ( 'NONE', #1872, 1000.000000000000000 ) ;
#9414=ORIENTED_EDGE ( 'NONE', *, *, #2350, .F. ) ;
#9425=FACE_OUTER_BOUND ( 'NONE', #7881, .T. ) ;
#9427=DIRECTION ( 'NONE',  ( -4.433365283261159518E-17, 1.000000000000000000, 0.000000000000000000 ) ) ;
#9449=VECTOR ( 'NONE', #8898, 1000.000000000000000 ) ;
#9457=VERTEX_POINT ( 'NONE', #1823 ) ;
#9458=DIRECTION ( 'NONE',  ( 1.850371707708589879E-16, -1.000000000000000000, 0.000000000000000000 ) ) ;
#9462=EDGE_LOOP ( 'NONE', ( #11247, #15651, #9246, #854, #17587, #16675, #2837, #14721, #11917, #14918, #17583, #3507, #6883, #12697, #8165, #11216 ) ) ;
#9484=ADVANCED_FACE ( 'NONE', ( #4676 ), #15991, .T. ) ;
#9496=DIRECTION ( 'NONE',  ( 0.000000000000000000, 0.000000000000000000, 1.000000000000000000 ) ) ;
#9516=EDGE_CURVE ( 'NONE', #4993, #14289, #14863, .T. ) ;
#9520=CARTESIAN_POINT ( 'NONE',  ( 8.785293332290788772E-16, 10.80000000000000071, 7.599999999999999645 ) ) ;
#9528=ADVANCED_FACE ( 'NONE', ( #975 ), #13466, .T. ) ;
#9532=DIRECTION ( 'NONE',  ( -1.000000000000000000, 0.000000000000000000, 0.000000000000000000 ) ) ;
#9539=CIRCLE ( 'NONE', #15030, 0.04999999999999969746 ) ;
#9543=DIRECTION ( 'NONE',  ( 0.000000000000000000, 0.000000000000000000, 1.000000000000000000 ) ) ;
#9545=DIRECTION ( 'NONE',  ( 1.000000000000000000, -2.220446049250309876E-16, -1.048990684667790150E-15 ) ) ;
#9551=UNCERTAINTY_MEASURE_WITH_UNIT (LENGTH_MEASURE( 1.000000000000000082E-05 ), #1746, 'distance_accuracy_value', 'NONE');
#9577=DIRECTION ( 'NONE',  ( 0.7071067811865470176, -0.7071067811865480168, 0.000000000000000000 ) ) ;
#9579=DIRECTION ( 'NONE',  ( -1.000000000000000000, 0.000000000000000000, 0.000000000000000000 ) ) ;
#9596=EDGE_CURVE ( 'NONE', #796, #5745, #9122, .T. ) ;
#9617=DIRECTION ( 'NONE',  ( -0.7071067811865475727, 0.7071067811865475727, 0.000000000000000000 ) ) ;
#9624=CARTESIAN_POINT ( 'NONE',  ( -1.699999999999999956, 9.299999999999998934, 7.599999999999999645 ) ) ;
#9630=ORIENTED_EDGE ( 'NONE', *, *, #13329, .T. ) ;
#9634=ORIENTED_EDGE ( 'NONE', *, *, #3826, .F. ) ;
#9653=CARTESIAN_POINT ( 'NONE',  ( -1.899999999999999911, 0.5999999999999999778, 7.599999999999999645 ) ) ;
#9659=VERTEX_POINT ( 'NONE', #14619 ) ;
#9660=DIRECTION ( 'NONE',  ( 1.000000000000000000, -2.220446049250319983E-16, 0.000000000000000000 ) ) ;
#9672=STYLED_ITEM ( 'NONE', ( #3065 ), #14083 ) ;
#9694=VECTOR ( 'NONE', #11341, 1000.000000000000000 ) ;
#9707=DIRECTION ( 'NONE',  ( 1.184237892933500047E-15, -1.000000000000000000, 0.000000000000000000 ) ) ;
#9738=CARTESIAN_POINT ( 'NONE',  ( 1.149999999999999911, 9.299999999999998934, 7.700000000000000178 ) ) ;
#9751=VECTOR ( 'NONE', #9579, 1000.000000000000000 ) ;
#9758=ADVANCED_FACE ( 'NONE', ( #7397 ), #13036, .T. ) ;
#9770=LINE ( 'NONE', #5418, #9751 ) ;
#9801=EDGE_LOOP ( 'NONE', ( #4813, #17671, #6926, #15590 ) ) ;
#9812=CARTESIAN_POINT ( 'NONE',  ( -1.899999999999999911, 11.40000000000000036, 6.599999999999999645 ) ) ;
#9821=EDGE_LOOP ( 'NONE', ( #2089, #2236, #11395, #2789 ) ) ;
#9834=CARTESIAN_POINT ( 'NONE',  ( 1.899999999999999911, 0.5999999999999999778, 7.700000000000000178 ) ) ;
#9855=ORIENTED_EDGE ( 'NONE', *, *, #2369, .T. ) ;
#9861=PLANE ( 'NONE',  #1767 ) ;
#9866=CARTESIAN_POINT ( 'NONE',  ( -1.800000000000000044, 11.40000000000000036, 6.599999999999999645 ) ) ;
#9888=DIRECTION ( 'NONE',  ( -9.349246523159200620E-16, 0.000000000000000000, -1.000000000000000000 ) ) ;
#9935=ORIENTED_EDGE ( 'NONE', *, *, #2064, .F. ) ;
#9966=AXIS2_PLACEMENT_3D ( 'NONE', #1121, #9545, #8254 ) ;
#9981=LINE ( 'NONE', #16919, #2166 ) ;
#9985=VERTEX_POINT ( 'NONE', #18071 ) ;
#10005=ORIENTED_EDGE ( 'NONE', *, *, #16944, .T. ) ;
#10008=EDGE_CURVE ( 'NONE', #17362, #2860, #9770, .T. ) ;
#10020=VECTOR ( 'NONE', #927, 1000.000000000000114 ) ;
#10027=CARTESIAN_POINT ( 'NONE',  ( -1.899999999999999911, 0.5999999999999999778, 6.599999999999999645 ) ) ;
#10044=FACE_OUTER_BOUND ( 'NONE', #3102, .T. ) ;
#10059=ADVANCED_FACE ( 'NONE', ( #4201 ), #9861, .T. ) ;
#10092=DIRECTION ( 'NONE',  ( 0.000000000000000000, 0.000000000000000000, -1.000000000000000000 ) ) ;
#10096=LINE ( 'NONE', #15746, #1428 ) ;
#10107=LINE ( 'NONE', #462, #6104 ) ;
#10126=ORIENTED_EDGE ( 'NONE', *, *, #1476, .F. ) ;
#10127=FACE_OUTER_BOUND ( 'NONE', #7026, .T. ) ;
#10143=CARTESIAN_POINT ( 'NONE',  ( 0.5999999999999999778, 0.5999999999999999778, 7.599999999999999645 ) ) ;
#10152=ADVANCED_FACE ( 'NONE', ( #15499 ), #14085, .T. ) ;
#10158=FACE_OUTER_BOUND ( 'NONE', #14245, .T. ) ;
#10160=DIRECTION ( 'NONE',  ( 0.000000000000000000, 1.000000000000000000, 0.000000000000000000 ) ) ;
#10171=ORIENTED_EDGE ( 'NONE', *, *, #1618, .F. ) ;
#10172=VERTEX_POINT ( 'NONE', #1416 ) ;
#10186=CARTESIAN_POINT ( 'NONE',  ( 0.5999999999999999778, 0.5999999999999999778, 7.599999999999999645 ) ) ;
#10194=ORIENTED_EDGE ( 'NONE', *, *, #13329, .F. ) ;
#10207=ORIENTED_EDGE ( 'NONE', *, *, #4729, .T. ) ;
#10211=EDGE_LOOP ( 'NONE', ( #12963, #695, #6150, #267 ) ) ;
#10221=VECTOR ( 'NONE', #16658, 1000.000000000000000 ) ;
#10227=ORIENTED_EDGE ( 'NONE', *, *, #6137, .T. ) ;
#10238=VERTEX_POINT ( 'NONE', #15687 ) ;
#10276=CARTESIAN_POINT ( 'NONE',  ( -1.699999999999999956, 9.299999999999998934, 7.700000000000000178 ) ) ;
#10291=AXIS2_PLACEMENT_3D ( 'NONE', #13423, #11574, #16111 ) ;
#10305=EDGE_LOOP ( 'NONE', ( #1584, #15655 ) ) ;
#10319=EDGE_CURVE ( 'NONE', #7625, #4727, #3254, .T. ) ;
#10330=ORIENTED_EDGE ( 'NONE', *, *, #16488, .T. ) ;
#10331=DIRECTION ( 'NONE',  ( 9.349246523159200620E-16, 0.000000000000000000, -1.000000000000000000 ) ) ;
#10334=CIRCLE ( 'NONE', #5621, 0.2750000000000000222 ) ;
#10336=DIRECTION ( 'NONE',  ( -1.000000000000000000, 0.000000000000000000, 0.000000000000000000 ) ) ;
#10346=PLANE ( 'NONE',  #17340 ) ;
#10373=ADVANCED_FACE ( 'NONE', ( #17485 ), #10454, .T. ) ;
#10385=LINE ( 'NONE', #17226, #5847 ) ;
#10406=CARTESIAN_POINT ( 'NONE',  ( 0.5999999999999999778, -7.347880794884110368E-17, 7.700000000000000178 ) ) ;
#10418=CARTESIAN_POINT ( 'NONE',  ( 1.800000000000000044, 0.5999999999999999778, 6.599999999999999645 ) ) ;
#10429=CIRCLE ( 'NONE', #7483, 0.04999999999999991257 ) ;
#10443=CARTESIAN_POINT ( 'NONE',  ( 4.225031457058369810E-16, 2.299999999999999822, 7.599999999999999645 ) ) ;
#10450=PLANE ( 'NONE',  #10291 ) ;
#10454=PLANE ( 'NONE',  #12409 ) ;
#10455=VERTEX_POINT ( 'NONE', #12416 ) ;
#10459=CIRCLE ( 'NONE', #6626, 0.5999999999999999778 ) ;
#10468=LINE ( 'NONE', #15867, #4927 ) ;
#10477=ORIENTED_EDGE ( 'NONE', *, *, #15498, .F. ) ;
#10490=LINE ( 'NONE', #8610, #5185 ) ;
#10501=DIRECTION ( 'NONE',  ( -9.349246523159200620E-16, 0.000000000000000000, -1.000000000000000000 ) ) ;
#10513=ADVANCED_FACE ( 'NONE', ( #8430 ), #16, .F. ) ;
#10527=AXIS2_PLACEMENT_3D ( 'NONE', #5872, #17059, #4549 ) ;
#10538=CARTESIAN_POINT ( 'NONE',  ( 1.750000000000000000, 11.40000000000000036, 7.550000000000000711 ) ) ;
#10565=ORIENTED_EDGE ( 'NONE', *, *, #12243, .F. ) ;
#10640=CARTESIAN_POINT ( 'NONE',  ( -0.9499999999999999556, 2.299999999999999822, 7.599999999999999645 ) ) ;
#10644=CARTESIAN_POINT ( 'NONE',  ( 1.149999999999999911, 9.248236190979499227, 7.693185165257809821 ) ) ;
#10655=DIRECTION ( 'NONE',  ( 0.000000000000000000, -0.2588190451025180749, 0.9659258262890690894 ) ) ;
#10656=VECTOR ( 'NONE', #5052, 1000.000000000000000 ) ;
#10663=ORIENTED_EDGE ( 'NONE', *, *, #215, .F. ) ;
#10673=DIRECTION ( 'NONE',  ( 1.000000000000000000, 0.000000000000000000, 0.000000000000000000 ) ) ;
#10697=ORIENTED_EDGE ( 'NONE', *, *, #15271, .F. ) ;
#10718=LINE ( 'NONE', #14790, #15887 ) ;
#10734=LINE ( 'NONE', #9333, #17974 ) ;
#10741=ADVANCED_FACE ( 'NONE', ( #16189 ), #1848, .T. ) ;
#10745=CARTESIAN_POINT ( 'NONE',  ( 1.149999999999999911, 6.472933199251450276, 6.846017351831609865 ) ) ;
#10753=EDGE_LOOP ( 'NONE', ( #13723, #183, #7392, #16083 ) ) ;
#10754=DIRECTION ( 'NONE',  ( 0.000000000000000000, 0.000000000000000000, 1.000000000000000000 ) ) ;
#10757=AXIS2_PLACEMENT_3D ( 'NONE', #629, #9323, #4786 ) ;
#10771=ORIENTED_EDGE ( 'NONE', *, *, #15271, .T. ) ;
#10788=DIRECTION ( 'NONE',  ( -1.000000000000000000, 0.000000000000000000, 0.000000000000000000 ) ) ;
#10808=FACE_OUTER_BOUND ( 'NONE', #4412, .T. ) ;
#10809=LINE ( 'NONE', #3769, #16532 ) ;
#10828=CIRCLE ( 'NONE', #8463, 0.1499999999999999667 ) ;
#10832=CARTESIAN_POINT ( 'NONE',  ( -1.750000000000000000, 11.40000000000000036, 7.599999999999999645 ) ) ;
#10842=CARTESIAN_POINT ( 'NONE',  ( -1.149999999999999911, 9.299999999999998934, 7.700000000000000178 ) ) ;
#10845=ORIENTED_EDGE ( 'NONE', *, *, #5048, .F. ) ;
#10866=EDGE_LOOP ( 'NONE', ( #16874, #141, #15223, #3309 ) ) ;
#10876=CARTESIAN_POINT ( 'NONE',  ( 0.9499999999999999556, 2.299999999999999822, 7.599999999999999645 ) ) ;
#10897=ORIENTED_EDGE ( 'NONE', *, *, #7682, .F. ) ;
#10907=VECTOR ( 'NONE', #2982, 1000.000000000000000 ) ;
#10914=DIRECTION ( 'NONE',  ( 1.000000000000000000, -1.224646799147350002E-16, 0.000000000000000000 ) ) ;
#10936=PLANE ( 'NONE',  #13179 ) ;
#10949=DIRECTION ( 'NONE',  ( 0.000000000000000000, 0.000000000000000000, -1.000000000000000000 ) ) ;
#10975=LINE ( 'NONE', #16622, #11133 ) ;
#10984=CARTESIAN_POINT ( 'NONE',  ( -0.5999999999999999778, 7.347880794884128857E-17, 7.599999999999999645 ) ) ;
#11010=CARTESIAN_POINT ( 'NONE',  ( 1.750000000000000000, 0.5999999999999999778, 7.700000000000000178 ) ) ;
#11026=CARTESIAN_POINT ( 'NONE',  ( 8.785293332290788772E-16, 10.80000000000000071, 7.700000000000000178 ) ) ;
#11033=FACE_OUTER_BOUND ( 'NONE', #5190, .T. ) ;
#11069=EDGE_CURVE ( 'NONE', #2860, #11926, #8058, .T. ) ;
#11073=CARTESIAN_POINT ( 'NONE',  ( -1.149999999999999911, 9.299999999999998934, 7.500000000000000000 ) ) ;
#11089=DIRECTION ( 'NONE',  ( 0.000000000000000000, 0.000000000000000000, 1.000000000000000000 ) ) ;
#11096=EDGE_CURVE ( 'NONE', #7698, #2828, #10334, .T. ) ;
#11119=FACE_OUTER_BOUND ( 'NONE', #1645, .T. ) ;
#11131=ORIENTED_EDGE ( 'NONE', *, *, #9352, .T. ) ;
#11133=VECTOR ( 'NONE', #12453, 1000.000000000000000 ) ;
#11141=VECTOR ( 'NONE', #1548, 1000.000000000000000 ) ;
#11142=ADVANCED_FACE ( 'NONE', ( #15548 ), #5613, .T. ) ;
#11145=DIRECTION ( 'NONE',  ( 2.261565420532729920E-16, 1.000000000000000000, 0.000000000000000000 ) ) ;
#11167=VECTOR ( 'NONE', #2925, 1000.000000000000000 ) ;
#11168=CARTESIAN_POINT ( 'NONE',  ( 0.5999999999999999778, -1.110223024625159992E-16, 7.599999999999999645 ) ) ;
#11189=ORIENTED_EDGE ( 'NONE', *, *, #17749, .F. ) ;
#11191=CARTESIAN_POINT ( 'NONE',  ( 0.000000000000000000, 0.000000000000000000, 0.000000000000000000 ) ) ;
#11192=VECTOR ( 'NONE', #10331, 1000.000000000000000 ) ;
#11203=AXIS2_PLACEMENT_3D ( 'NONE', #357, #3221, #3310 ) ;
#11211=ORIENTED_EDGE ( 'NONE', *, *, #8370, .T. ) ;
#11215=ORIENTED_EDGE ( 'NONE', *, *, #17956, .F. ) ;
#11216=ORIENTED_EDGE ( 'NONE', *, *, #4273, .F. ) ;
#11225=CARTESIAN_POINT ( 'NONE',  ( 1.800000000000000044, 8.881784197001260212E-17, 9.441371669411539713 ) ) ;
#11243=ORIENTED_EDGE ( 'NONE', *, *, #10008, .T. ) ;
#11247=ORIENTED_EDGE ( 'NONE', *, *, #4824, .T. ) ;
#11255=FACE_OUTER_BOUND ( 'NONE', #6944, .T. ) ;
#11262=ORIENTED_EDGE ( 'NONE', *, *, #6642, .T. ) ;
#11272=LINE ( 'NONE', #6833, #7587 ) ;
#11307=VECTOR ( 'NONE', #13582, 1000.000000000000000 ) ;
#11324=CARTESIAN_POINT ( 'NONE',  ( -1.149999999999999911, 9.248236190979499227, 7.693185165257809821 ) ) ;
#11326=ORIENTED_EDGE ( 'NONE', *, *, #14183, .F. ) ;
#11341=DIRECTION ( 'NONE',  ( 1.000000000000000000, -1.850371707708589879E-16, 0.000000000000000000 ) ) ;
#11368=CARTESIAN_POINT ( 'NONE',  ( 1.750000000000000000, 11.40000000000000036, 7.550000000000000711 ) ) ;
#11377=LINE ( 'NONE', #1376, #7028 ) ;
#11391=EDGE_LOOP ( 'NONE', ( #16495, #2726, #2535, #3026 ) ) ;
#11395=ORIENTED_EDGE ( 'NONE', *, *, #17989, .F. ) ;
#11400=DIRECTION ( 'NONE',  ( -1.000000000000000000, 0.000000000000000000, 0.000000000000000000 ) ) ;
#11444=LINE ( 'NONE', #15719, #9343 ) ;
#11447=VECTOR ( 'NONE', #17718, 1000.000000000000000 ) ;
#11449=ORIENTED_EDGE ( 'NONE', *, *, #16488, .F. ) ;
#11458=EDGE_LOOP ( 'NONE', ( #17064, #2464, #2018, #8656 ) ) ;
#11480=ORIENTED_EDGE ( 'NONE', *, *, #16707, .T. ) ;
#11503=ORIENTED_EDGE ( 'NONE', *, *, #14242, .F. ) ;
#11517=DIRECTION ( 'NONE',  ( 0.000000000000000000, 6.055990775824630636E-30, -1.000000000000000000 ) ) ;
#11543=LINE ( 'NONE', #6250, #11933 ) ;
#11554=LINE ( 'NONE', #443, #15329 ) ;
#11574=DIRECTION ( 'NONE',  ( -2.220446049250309876E-16, -1.000000000000000000, 5.551115123125800057E-15 ) ) ;
#11595=VECTOR ( 'NONE', #18198, 1000.000000000000000 ) ;
#11598=CARTESIAN_POINT ( 'NONE',  ( 0.5999999999999999778, 11.40000000000000036, 7.599999999999999645 ) ) ;
#11600=CARTESIAN_POINT ( 'NONE',  ( -0.5999999999999999778, 0.5999999999999999778, 7.700000000000000178 ) ) ;
#11621=DIRECTION ( 'NONE',  ( 0.000000000000000000, -1.836189155707839943E-31, -1.000000000000000000 ) ) ;
#11623=ORIENTED_EDGE ( 'NONE', *, *, #1552, .F. ) ;
#11624=EDGE_CURVE ( 'NONE', #4443, #4993, #16544, .T. ) ;
#11637=LINE ( 'NONE', #3218, #3747 ) ;
#11655=VERTEX_POINT ( 'NONE', #17996 ) ;
#11659=ORIENTED_EDGE ( 'NONE', *, *, #6195, .F. ) ;
#11703=EDGE_CURVE ( 'NONE', #2916, #16779, #5342, .T. ) ;
#11735=DIRECTION ( 'NONE',  ( 0.000000000000000000, 0.000000000000000000, -1.000000000000000000 ) ) ;
#11755=ORIENTED_EDGE ( 'NONE', *, *, #5180, .F. ) ;
#11756=CARTESIAN_POINT ( 'NONE',  ( -1.899999999999999911, 11.40000000000000036, 7.550000000000000711 ) ) ;
#11784=ORIENTED_EDGE ( 'NONE', *, *, #90, .F. ) ;
#11785=CYLINDRICAL_SURFACE ( 'NONE', #15071, 0.1499999999999999667 ) ;
#11802=AXIS2_PLACEMENT_3D ( 'NONE', #3294, #13189, #9496 ) ;
#11803=DIRECTION ( 'NONE',  ( 1.000000000000000000, 0.000000000000000000, 0.000000000000000000 ) ) ;
#11830=CARTESIAN_POINT ( 'NONE',  ( -1.750000000000000000, 0.5999999999999999778, 7.550000000000000711 ) ) ;
#11873=LINE ( 'NONE', #8986, #12966 ) ;
#11888=ORIENTED_EDGE ( 'NONE', *, *, #16146, .T. ) ;
#11903=ORIENTED_EDGE ( 'NONE', *, *, #15041, .T. ) ;
#11917=ORIENTED_EDGE ( 'NONE', *, *, #1809, .F. ) ;
#11926=VERTEX_POINT ( 'NONE', #5453 ) ;
#11933=VECTOR ( 'NONE', #17448, 1000.000000000000000 ) ;
#11967=ADVANCED_FACE ( 'NONE', ( #12575 ), #4233, .F. ) ;
#11981=ORIENTED_EDGE ( 'NONE', *, *, #10319, .F. ) ;
#11994=PLANE ( 'NONE',  #6763 ) ;
#12009=AXIS2_PLACEMENT_3D ( 'NONE', #17711, #3740, #8780 ) ;
#12017=ORIENTED_EDGE ( 'NONE', *, *, #5976, .F. ) ;
#12025=VECTOR ( 'NONE', #10673, 1000.000000000000000 ) ;
#12029=FACE_OUTER_BOUND ( 'NONE', #17427, .T. ) ;
#12048=CARTESIAN_POINT ( 'NONE',  ( 0.5999999999999999778, 0.5999999999999999778, 7.599999999999999645 ) ) ;
#12060=CARTESIAN_POINT ( 'NONE',  ( 1.750000000000000000, 0.5999999999999999778, 7.550000000000000711 ) ) ;
#12079=VECTOR ( 'NONE', #6298, 1000.000000000000000 ) ;
#12083=EDGE_CURVE ( 'NONE', #1492, #7108, #4579, .T. ) ;
#12098=LINE ( 'NONE', #3651, #11447 ) ;
#12104=ORIENTED_EDGE ( 'NONE', *, *, #1887, .F. ) ;
#12124=LINE ( 'NONE', #17548, #4624 ) ;
#12130=FACE_OUTER_BOUND ( 'NONE', #16049, .T. ) ;
#12154=DIRECTION ( 'NONE',  ( 0.000000000000000000, 0.000000000000000000, 1.000000000000000000 ) ) ;
#12159=CARTESIAN_POINT ( 'NONE',  ( 3.371799150351489833E-16, 2.299999999999999822, 7.599999999999999645 ) ) ;
#12172=VERTEX_POINT ( 'NONE', #3307 ) ;
#12177=CARTESIAN_POINT ( 'NONE',  ( -1.750000000000000000, 11.40000000000000036, 7.700000000000000178 ) ) ;
#12206=LINE ( 'NONE', #2302, #7378 ) ;
#12209=EDGE_CURVE ( 'NONE', #11655, #2611, #17443, .T. ) ;
#12218=LINE ( 'NONE', #11010, #10221 ) ;
#12235=PLANE ( 'NONE',  #8108 ) ;
#12243=EDGE_CURVE ( 'NONE', #2692, #8647, #4772, .T. ) ;
#12244=DIRECTION ( 'NONE',  ( -1.000000000000000000, 0.000000000000000000, 0.000000000000000000 ) ) ;
#12256=LINE ( 'NONE', #12618, #15057 ) ;
#12266=DIRECTION ( 'NONE',  ( -1.000000000000000000, 0.000000000000000000, 0.000000000000000000 ) ) ;
#12271=ORIENTED_EDGE ( 'NONE', *, *, #14345, .T. ) ;
#12334=DIRECTION ( 'NONE',  ( 1.903239470785979823E-16, 1.000000000000000000, 0.000000000000000000 ) ) ;
#12358=ORIENTED_EDGE ( 'NONE', *, *, #108, .F. ) ;
#12384=VECTOR ( 'NONE', #12667, 1000.000000000000000 ) ;
#12390=CARTESIAN_POINT ( 'NONE',  ( -0.5999999999999999778, 7.347880794884128857E-17, 7.599999999999999645 ) ) ;
#12400=ORIENTED_EDGE ( 'NONE', *, *, #3826, .T. ) ;
#12409=AXIS2_PLACEMENT_3D ( 'NONE', #7692, #13338, #650 ) ;
#12413=FACE_OUTER_BOUND ( 'NONE', #3911, .T. ) ;
#12416=CARTESIAN_POINT ( 'NONE',  ( -0.5999999999999999778, 11.40000000000000036, 7.599999999999999645 ) ) ;
#12453=DIRECTION ( 'NONE',  ( 1.000000000000000000, -1.224646799147350002E-16, 0.000000000000000000 ) ) ;
#12457=DIRECTION ( 'NONE',  ( 1.000000000000000000, 0.000000000000000000, 0.000000000000000000 ) ) ;
#12462=ADVANCED_FACE ( 'NONE', ( #16444 ), #3753, .T. ) ;
#12484=DIRECTION ( 'NONE',  ( 0.000000000000000000, 0.000000000000000000, 1.000000000000000000 ) ) ;
#12489=CYLINDRICAL_SURFACE ( 'NONE', #15891, 0.2750000000000000222 ) ;
#12516=FACE_OUTER_BOUND ( 'NONE', #17196, .T. ) ;
#12529=DIRECTION ( 'NONE',  ( 0.000000000000000000, 0.000000000000000000, 1.000000000000000000 ) ) ;
#12539=ORIENTED_EDGE ( 'NONE', *, *, #5876, .T. ) ;
#12570=CYLINDRICAL_SURFACE ( 'NONE', #3056, 0.1499999999999999667 ) ;
#12575=FACE_OUTER_BOUND ( 'NONE', #5568, .T. ) ;
#12577=DIRECTION ( 'NONE',  ( -2.261565420532729920E-16, -1.000000000000000000, 0.000000000000000000 ) ) ;
#12586=CARTESIAN_POINT ( 'NONE',  ( -1.699999999999999956, 2.299999999999999822, 7.700000000000000178 ) ) ;
#12618=CARTESIAN_POINT ( 'NONE',  ( 1.300000000000000044, -1.592040838891560081E-16, 7.700000000000000178 ) ) ;
#12619=AXIS2_PLACEMENT_3D ( 'NONE', #3486, #16181, #9427 ) ;
#12629=PLANE ( 'NONE',  #5814 ) ;
#12649=VECTOR ( 'NONE', #5765, 1000.000000000000000 ) ;
#12662=VECTOR ( 'NONE', #16012, 1000.000000000000000 ) ;
#12663=VECTOR ( 'NONE', #12577, 1000.000000000000000 ) ;
#12664=CARTESIAN_POINT ( 'NONE',  ( 1.149999999999999911, 9.274118095489749081, 7.596592582628910684 ) ) ;
#12667=DIRECTION ( 'NONE',  ( -1.903239470785979823E-16, -1.000000000000000000, 0.000000000000000000 ) ) ;
#12675=VERTEX_POINT ( 'NONE', #9382 ) ;
#12697=ORIENTED_EDGE ( 'NONE', *, *, #9352, .F. ) ;
#12708=DIRECTION ( 'NONE',  ( 0.000000000000000000, 0.000000000000000000, 1.000000000000000000 ) ) ;
#12717=LINE ( 'NONE', #11324, #14426 ) ;
#12730=FACE_OUTER_BOUND ( 'NONE', #17252, .T. ) ;
#12740=EDGE_CURVE ( 'NONE', #7150, #17150, #15125, .T. ) ;
#12768=ORIENTED_EDGE ( 'NONE', *, *, #5419, .T. ) ;
#12806=LINE ( 'NONE', #10186, #12649 ) ;
#12822=CARTESIAN_POINT ( 'NONE',  ( -1.899999999999999911, 0.5999999999999999778, 7.599999999999999645 ) ) ;
#12846=CARTESIAN_POINT ( 'NONE',  ( 1.899999999999999911, 0.5999999999999999778, 7.550000000000000711 ) ) ;
#12849=ORIENTED_EDGE ( 'NONE', *, *, #13471, .F. ) ;
#12852=( NAMED_UNIT ( * ) SI_UNIT ( $, .STERADIAN. ) SOLID_ANGLE_UNIT ( ) );
#12859=CARTESIAN_POINT ( 'NONE',  ( -1.899999999999999911, 0.5999999999999999778, 7.700000000000000178 ) ) ;
#12867=EDGE_LOOP ( 'NONE', ( #6056, #11888, #3703, #8597, #4578, #9630, #7136, #2949 ) ) ;
#12872=ORIENTED_EDGE ( 'NONE', *, *, #8105, .F. ) ;
#12881=DIRECTION ( 'NONE',  ( 0.000000000000000000, 0.000000000000000000, -1.000000000000000000 ) ) ;
#12897=EDGE_CURVE ( 'NONE', #6428, #17362, #8085, .T. ) ;
#12902=VECTOR ( 'NONE', #280, 1000.000000000000000 ) ;
#12917=LINE ( 'NONE', #245, #3797 ) ;
#12918=EDGE_CURVE ( 'NONE', #8002, #2860, #16762, .T. ) ;
#12938=VERTEX_POINT ( 'NONE', #16596 ) ;
#12952=AXIS2_PLACEMENT_3D ( 'NONE', #990, #13681, #6627 ) ;
#12963=ORIENTED_EDGE ( 'NONE', *, *, #148, .T. ) ;
#12965=CARTESIAN_POINT ( 'NONE',  ( 1.800000000000000044, 11.40000000000000036, 7.550000000000000711 ) ) ;
#12966=VECTOR ( 'NONE', #2238, 1000.000000000000114 ) ;
#12999=CARTESIAN_POINT ( 'NONE',  ( -1.300000000000000044, 1.592040838891560081E-16, 7.599999999999999645 ) ) ;
#13036=PLANE ( 'NONE',  #11203 ) ;
#13039=CARTESIAN_POINT ( 'NONE',  ( -1.149999999999999911, 9.299999999999998934, 7.700000000000000178 ) ) ;
#13070=CARTESIAN_POINT ( 'NONE',  ( -1.800000000000000044, 11.40000000000000036, 6.599999999999999645 ) ) ;
#13075=ORIENTED_EDGE ( 'NONE', *, *, #86, .F. ) ;
#13087=EDGE_LOOP ( 'NONE', ( #14875, #15834, #6433, #14554 ) ) ;
#13111=CYLINDRICAL_SURFACE ( 'NONE', #5412, 0.04999999999999969746 ) ;
#13125=DIRECTION ( 'NONE',  ( -1.000000000000000000, 0.000000000000000000, 0.000000000000000000 ) ) ;
#13179=AXIS2_PLACEMENT_3D ( 'NONE', #15114, #7977, #9543 ) ;
#13183=VERTEX_POINT ( 'NONE', #16370 ) ;
#13189=DIRECTION ( 'NONE',  ( -1.000000000000000000, 0.000000000000000000, 0.000000000000000000 ) ) ;
#13192=EDGE_LOOP ( 'NONE', ( #4827, #14016, #865, #18188 ) ) ;
#13196=ORIENTED_EDGE ( 'NONE', *, *, #4194, .F. ) ;
#13198=CARTESIAN_POINT ( 'NONE',  ( -0.5999999999999999778, 11.40000000000000036, 7.599999999999999645 ) ) ;
#13205=SHAPE_REPRESENTATION_RELATIONSHIP ( 'NONE' , 'NONE' ,  #2146, #15507 ) ;
#13206=VECTOR ( 'NONE', #1310, 1000.000000000000000 ) ;
#13213=DIRECTION ( 'NONE',  ( -2.220446049250309876E-16, -1.000000000000000000, -2.902774059941839988E-17 ) ) ;
#13229=CARTESIAN_POINT ( 'NONE',  ( -1.149999999999999911, 9.299999999999998934, 7.599999999999999645 ) ) ;
#13245=CARTESIAN_POINT ( 'NONE',  ( 1.149999999999999911, 6.447051294741199534, 6.942609934460510779 ) ) ;
#13283=DIRECTION ( 'NONE',  ( -1.850371707708589879E-16, -1.000000000000000000, 0.000000000000000000 ) ) ;
#13298=DIRECTION ( 'NONE',  ( 0.000000000000000000, -0.2588190451025180749, 0.9659258262890690894 ) ) ;
#13329=EDGE_CURVE ( 'NONE', #16159, #13183, #8408, .T. ) ;
#13338=DIRECTION ( 'NONE',  ( -0.000000000000000000, 1.000000000000000000, 0.000000000000000000 ) ) ;
#13374=CARTESIAN_POINT ( 'NONE',  ( -1.750000000000000000, 11.40000000000000036, 7.700000000000000178 ) ) ;
#13378=FACE_BOUND ( 'NONE', #1562, .T. ) ;
#13388=ORIENTED_EDGE ( 'NONE', *, *, #15041, .F. ) ;
#13392=ORIENTED_EDGE ( 'NONE', *, *, #7104, .F. ) ;
#13401=LINE ( 'NONE', #1776, #18280 ) ;
#13403=ORIENTED_EDGE ( 'NONE', *, *, #7449, .T. ) ;
#13415=DIRECTION ( 'NONE',  ( 1.000000000000000000, -1.224646799147350002E-16, 0.000000000000000000 ) ) ;
#13423=CARTESIAN_POINT ( 'NONE',  ( -1.750000000000000000, 0.5999999999999999778, 7.700000000000000178 ) ) ;
#13451=EDGE_LOOP ( 'NONE', ( #1319, #3455, #9414, #13741 ) ) ;
#13466=PLANE ( 'NONE',  #17688 ) ;
#13468=VERTEX_POINT ( 'NONE', #4493 ) ;
#13471=EDGE_CURVE ( 'NONE', #3917, #4727, #15802, .T. ) ;
#13480=ORIENTED_EDGE ( 'NONE', *, *, #12243, .T. ) ;
#13482=DIRECTION ( 'NONE',  ( 2.055968564120659776E-16, 1.000000000000000000, 0.000000000000000000 ) ) ;
#13490=AXIS2_PLACEMENT_3D ( 'NONE', #15665, #8694, #10092 ) ;
#13493=CYLINDRICAL_SURFACE ( 'NONE', #15906, 0.5999999999999999778 ) ;
#13527=EDGE_LOOP ( 'NONE', ( #15415, #17184, #5006, #3682 ) ) ;
#13573=CARTESIAN_POINT ( 'NONE',  ( 4.225031457058369810E-16, 2.299999999999999822, 7.700000000000000178 ) ) ;
#13582=DIRECTION ( 'NONE',  ( 0.7071067811865470176, -0.7071067811865480168, 0.000000000000000000 ) ) ;
#13615=LINE ( 'NONE', #8065, #10020 ) ;
#13653=ADVANCED_FACE ( 'NONE', ( #13378, #693, #6330 ), #11994, .F. ) ;
#13681=DIRECTION ( 'NONE',  ( -0.000000000000000000, 1.000000000000000000, 0.000000000000000000 ) ) ;
#13682=CYLINDRICAL_SURFACE ( 'NONE', #2281, 0.1000000000000002554 ) ;
#13689=PLANE ( 'NONE',  #14695 ) ;
#13721=ORIENTED_EDGE ( 'NONE', *, *, #5902, .T. ) ;
#13723=ORIENTED_EDGE ( 'NONE', *, *, #2695, .T. ) ;
#13741=ORIENTED_EDGE ( 'NONE', *, *, #1665, .T. ) ;
#13753=DIRECTION ( 'NONE',  ( 0.000000000000000000, 0.000000000000000000, 1.000000000000000000 ) ) ;
#13778=ORIENTED_EDGE ( 'NONE', *, *, #16166, .T. ) ;
#13782=DIRECTION ( 'NONE',  ( -2.261565420532729920E-16, -1.000000000000000000, 0.000000000000000000 ) ) ;
#13783=VECTOR ( 'NONE', #12266, 1000.000000000000000 ) ;
#13795=AXIS2_PLACEMENT_3D ( 'NONE', #2264, #972, #8019 ) ;
#13816=DIRECTION ( 'NONE',  ( -1.000000000000000000, 0.000000000000000000, 0.000000000000000000 ) ) ;
#13841=DIRECTION ( 'NONE',  ( 0.000000000000000000, 0.000000000000000000, -1.000000000000000000 ) ) ;
#13845=PLANE ( 'NONE',  #15179 ) ;
#13847=VECTOR ( 'NONE', #2028, 1000.000000000000000 ) ;
#13858=DIRECTION ( 'NONE',  ( 0.000000000000000000, 0.000000000000000000, 1.000000000000000000 ) ) ;
#13890=CARTESIAN_POINT ( 'NONE',  ( -0.5999999999999999778, 10.80000000000000071, 7.599999999999999645 ) ) ;
#13896=ORIENTED_EDGE ( 'NONE', *, *, #2191, .T. ) ;
#13908=EDGE_CURVE ( 'NONE', #5745, #796, #2292, .T. ) ;
#13922=ORIENTED_EDGE ( 'NONE', *, *, #2634, .T. ) ;
#13939=DIRECTION ( 'NONE',  ( -0.000000000000000000, 1.000000000000000000, 0.000000000000000000 ) ) ;
#13942=ORIENTED_EDGE ( 'NONE', *, *, #15636, .F. ) ;
#13956=ORIENTED_EDGE ( 'NONE', *, *, #12918, .T. ) ;
#13965=CARTESIAN_POINT ( 'NONE',  ( 0.5999999999999999778, -7.347880794884110368E-17, 7.599999999999999645 ) ) ;
#13978=VERTEX_POINT ( 'NONE', #9834 ) ;
#13979=CARTESIAN_POINT ( 'NONE',  ( -1.750000000000000000, 11.40000000000000036, 7.550000000000000711 ) ) ;
#13982=EDGE_LOOP ( 'NONE', ( #16974, #11189, #2586, #9855 ) ) ;
#13996=ADVANCED_FACE ( 'NONE', ( #12516 ), #18224, .F. ) ;
#14003=ORIENTED_EDGE ( 'NONE', *, *, #4380, .F. ) ;
#14014=CARTESIAN_POINT ( 'NONE',  ( -1.800000000000000044, 11.40000000000000036, 7.550000000000000711 ) ) ;
#14016=ORIENTED_EDGE ( 'NONE', *, *, #5567, .T. ) ;
#14047=CARTESIAN_POINT ( 'NONE',  ( -1.750000000000000000, 0.5999999999999999778, 7.550000000000000711 ) ) ;
#14083=MANIFOLD_SOLID_BREP ( 'Stock-MAS-687-1', #197 ) ;
#14085=PLANE ( 'NONE',  #17701 ) ;
#14108=CARTESIAN_POINT ( 'NONE',  ( 1.800000000000000044, 0.5999999999999999778, 7.550000000000000711 ) ) ;
#14132=CARTESIAN_POINT ( 'NONE',  ( -1.149999999999999911, 6.447051294741199534, 6.942609934460510779 ) ) ;
#14183=EDGE_CURVE ( 'NONE', #404, #9178, #11377, .T. ) ;
#14190=CARTESIAN_POINT ( 'NONE',  ( -1.149999999999999911, 6.472933199251450276, 6.846017351831609865 ) ) ;
#14201=ORIENTED_EDGE ( 'NONE', *, *, #2191, .F. ) ;
#14212=FACE_OUTER_BOUND ( 'NONE', #13451, .T. ) ;
#14213=DIRECTION ( 'NONE',  ( -2.917038411497409743E-62, -1.000000000000000000, 1.836189155707839943E-31 ) ) ;
#14234=ADVANCED_FACE ( 'NONE', ( #3123 ), #10346, .T. ) ;
#14242=EDGE_CURVE ( 'NONE', #14289, #6043, #14520, .T. ) ;
#14245=EDGE_LOOP ( 'NONE', ( #8621, #17451, #14201, #10565 ) ) ;
#14260=CARTESIAN_POINT ( 'NONE',  ( -0.5999999999999999778, 10.80000000000000071, 7.700000000000000178 ) ) ;
#14289=VERTEX_POINT ( 'NONE', #17104 ) ;
#14297=PLANE ( 'NONE',  #5526 ) ;
#14345=EDGE_CURVE ( 'NONE', #15079, #1993, #4509, .T. ) ;
#14353=EDGE_CURVE ( 'NONE', #6043, #9985, #3046, .T. ) ;
#14365=EDGE_CURVE ( 'NONE', #2448, #8002, #17370, .T. ) ;
#14407=VERTEX_POINT ( 'NONE', #8048 ) ;
#14418=VECTOR ( 'NONE', #8110, 1000.000000000000000 ) ;
#14426=VECTOR ( 'NONE', #5679, 1000.000000000000114 ) ;
#14427=CARTESIAN_POINT ( 'NONE',  ( -1.800000000000000044, 11.40000000000000036, 7.550000000000000711 ) ) ;
#14428=DIRECTION ( 'NONE',  ( 0.000000000000000000, 0.000000000000000000, -1.000000000000000000 ) ) ;
#14453=CIRCLE ( 'NONE', #7655, 0.5999999999999999778 ) ;
#14460=EDGE_CURVE ( 'NONE', #2692, #7150, #17630, .T. ) ;
#14482=DIRECTION ( 'NONE',  ( 5.551115123125880521E-15, -1.000000000000000000, -6.055990775824630636E-30 ) ) ;
#14502=ORIENTED_EDGE ( 'NONE', *, *, #3366, .T. ) ;
#14520=LINE ( 'NONE', #12859, #5232 ) ;
#14524=CARTESIAN_POINT ( 'NONE',  ( 4.225031457058369810E-16, 2.299999999999999822, 7.599999999999999645 ) ) ;
#14533=ADVANCED_FACE ( 'NONE', ( #16555 ), #3576, .F. ) ;
#14550=VECTOR ( 'NONE', #11145, 1000.000000000000000 ) ;
#14553=ADVANCED_FACE ( 'NONE', ( #16178 ), #13493, .F. ) ;
#14554=ORIENTED_EDGE ( 'NONE', *, *, #15815, .F. ) ;
#14558=CARTESIAN_POINT ( 'NONE',  ( -1.699999999999999956, 9.299999999999998934, 7.599999999999999645 ) ) ;
#14570=ORIENTED_EDGE ( 'NONE', *, *, #3260, .F. ) ;
#14573=VECTOR ( 'NONE', #9888, 1000.000000000000000 ) ;
#14576=ORIENTED_EDGE ( 'NONE', *, *, #6504, .T. ) ;
#14577=ADVANCED_FACE ( 'NONE', ( #9425 ), #13689, .F. ) ;
#14590=DIRECTION ( 'NONE',  ( 0.000000000000000000, 0.2588190451025180749, -0.9659258262890690894 ) ) ;
#14594=ORIENTED_EDGE ( 'NONE', *, *, #1887, .T. ) ;
#14598=ORIENTED_EDGE ( 'NONE', *, *, #16944, .F. ) ;
#14609=FACE_OUTER_BOUND ( 'NONE', #3197, .T. ) ;
#14618=VECTOR ( 'NONE', #3806, 1000.000000000000114 ) ;
#14619=CARTESIAN_POINT ( 'NONE',  ( -0.5999999999999999778, 10.80000000000000071, 7.599999999999999645 ) ) ;
#14622=LINE ( 'NONE', #1937, #2551 ) ;
#14660=DIRECTION ( 'NONE',  ( 2.220446049250309876E-16, 1.000000000000000000, 0.000000000000000000 ) ) ;
#14676=EDGE_LOOP ( 'NONE', ( #3719, #1617, #62, #2977 ) ) ;
#14677=DIRECTION ( 'NONE',  ( 0.000000000000000000, 0.000000000000000000, 1.000000000000000000 ) ) ;
#14679=DIRECTION ( 'NONE',  ( 1.000000000000000000, 0.000000000000000000, 0.000000000000000000 ) ) ;
#14681=ORIENTED_EDGE ( 'NONE', *, *, #17766, .F. ) ;
#14695=AXIS2_PLACEMENT_3D ( 'NONE', #15089, #2484, #1460 ) ;
#14721=ORIENTED_EDGE ( 'NONE', *, *, #8733, .F. ) ;
#14728=EDGE_LOOP ( 'NONE', ( #393, #14681, #5667, #7898 ) ) ;
#14736=CARTESIAN_POINT ( 'NONE',  ( -1.750000000000000000, 11.40000000000000036, 7.550000000000000711 ) ) ;
#14742=CARTESIAN_POINT ( 'NONE',  ( 1.800000000000000044, 0.5999999999999999778, 6.599999999999999645 ) ) ;
#14747=VECTOR ( 'NONE', #17604, 1000.000000000000000 ) ;
#14773=CARTESIAN_POINT ( 'NONE',  ( -1.750000000000000000, 11.40000000000000036, 7.599999999999999645 ) ) ;
#14790=CARTESIAN_POINT ( 'NONE',  ( -0.5999999999999999778, 7.347880794884128857E-17, 7.700000000000000178 ) ) ;
#14795=DIRECTION ( 'NONE',  ( -1.000000000000000000, 0.000000000000000000, 0.000000000000000000 ) ) ;
#14799=PLANE ( 'NONE',  #2319 ) ;
#14805=ORIENTED_EDGE ( 'NONE', *, *, #7682, .T. ) ;
#14834=PRODUCT_CONTEXT ( 'NONE', #830, 'mechanical' ) ;
#14863=LINE ( 'NONE', #13374, #14747 ) ;
#14875=ORIENTED_EDGE ( 'NONE', *, *, #639, .T. ) ;
#14878=LINE ( 'NONE', #4862, #16497 ) ;
#14880=ORIENTED_EDGE ( 'NONE', *, *, #16707, .F. ) ;
#14893=CARTESIAN_POINT ( 'NONE',  ( 1.149999999999999911, 9.299999999999998934, 7.500000000000000000 ) ) ;
#14901=DIRECTION ( 'NONE',  ( 0.000000000000000000, 0.000000000000000000, 1.000000000000000000 ) ) ;
#14918=ORIENTED_EDGE ( 'NONE', *, *, #5298, .T. ) ;
#14923=VECTOR ( 'NONE', #8061, 1000.000000000000000 ) ;
#14941=ORIENTED_EDGE ( 'NONE', *, *, #17749, .T. ) ;
#14954=PLANE ( 'NONE',  #13795 ) ;
#14959=EDGE_CURVE ( 'NONE', #9457, #5374, #11444, .T. ) ;
#14961=VERTEX_POINT ( 'NONE', #6058 ) ;
#15002=VECTOR ( 'NONE', #7580, 1000.000000000000000 ) ;
#15003=ORIENTED_EDGE ( 'NONE', *, *, #11069, .T. ) ;
#15013=DIRECTION ( 'NONE',  ( -7.656710514656250048E-17, 0.9659258262890690894, 0.2588190451025180749 ) ) ;
#15020=FACE_OUTER_BOUND ( 'NONE', #11458, .T. ) ;
#15030=AXIS2_PLACEMENT_3D ( 'NONE', #5783, #14213, #8383 ) ;
#15041=EDGE_CURVE ( 'NONE', #1835, #15121, #3449, .T. ) ;
#15057=VECTOR ( 'NONE', #6970, 1000.000000000000000 ) ;
#15062=FACE_OUTER_BOUND ( 'NONE', #493, .T. ) ;
#15071=AXIS2_PLACEMENT_3D ( 'NONE', #5103, #6929, #10754 ) ;
#15079=VERTEX_POINT ( 'NONE', #17704 ) ;
#15080=CARTESIAN_POINT ( 'NONE',  ( 1.110223024625159893E-15, 0.3005290370886140594, 5.295654259262600583 ) ) ;
#15089=CARTESIAN_POINT ( 'NONE',  ( -1.899999999999999911, 0.5999999999999999778, 7.599999999999999645 ) ) ;
#15105=CARTESIAN_POINT ( 'NONE',  ( 1.149999999999999911, 6.447051294741199534, 6.942609934460510779 ) ) ;
#15114=CARTESIAN_POINT ( 'NONE',  ( -1.699999999999999956, 9.299999999999998934, 7.599999999999999645 ) ) ;
#15121=VERTEX_POINT ( 'NONE', #3639 ) ;
#15125=LINE ( 'NONE', #2342, #8027 ) ;
#15129=CARTESIAN_POINT ( 'NONE',  ( 0.9499999999999999556, 2.299999999999999822, 7.599999999999999645 ) ) ;
#15154=FACE_OUTER_BOUND ( 'NONE', #7987, .T. ) ;
#15163=VECTOR ( 'NONE', #10336, 1000.000000000000000 ) ;
#15178=DIRECTION ( 'NONE',  ( 0.000000000000000000, 0.000000000000000000, -1.000000000000000000 ) ) ;
#15179=AXIS2_PLACEMENT_3D ( 'NONE', #9866, #16705, #1166 ) ;
#15193=ORIENTED_EDGE ( 'NONE', *, *, #7449, .F. ) ;
#15223=ORIENTED_EDGE ( 'NONE', *, *, #3966, .F. ) ;
#15243=CARTESIAN_POINT ( 'NONE',  ( -1.899999999999999911, 0.5999999999999999778, 7.550000000000000711 ) ) ;
#15248=DIRECTION ( 'NONE',  ( 9.349246523159210481E-16, 0.000000000000000000, 1.000000000000000000 ) ) ;
#15250=ORIENTED_EDGE ( 'NONE', *, *, #11096, .T. ) ;
#15251=DIRECTION ( 'NONE',  ( -1.000000000000000000, 2.381191005321109844E-32, 0.000000000000000000 ) ) ;
#15271=EDGE_CURVE ( 'NONE', #4902, #6049, #10975, .T. ) ;
#15284=LINE ( 'NONE', #9624, #2579 ) ;
#15290=ADVANCED_FACE ( 'NONE', ( #2538 ), #12629, .T. ) ;
#15329=VECTOR ( 'NONE', #6083, 1000.000000000000000 ) ;
#15330=VECTOR ( 'NONE', #1435, 1000.000000000000000 ) ;
#15384=ADVANCED_FACE ( 'NONE', ( #10127 ), #14297, .T. ) ;
#15399=ORIENTED_EDGE ( 'NONE', *, *, #8370, .F. ) ;
#15401=ORIENTED_EDGE ( 'NONE', *, *, #4824, .F. ) ;
#15415=ORIENTED_EDGE ( 'NONE', *, *, #5419, .F. ) ;
#15436=ORIENTED_EDGE ( 'NONE', *, *, #16825, .F. ) ;
#15447=ADVANCED_FACE ( 'NONE', ( #14212 ), #15609, .T. ) ;
#15462=ADVANCED_FACE ( 'NONE', ( #10044 ), #1706, .T. ) ;
#15498=EDGE_CURVE ( 'NONE', #11926, #13468, #2562, .T. ) ;
#15499=FACE_OUTER_BOUND ( 'NONE', #9821, .T. ) ;
#15507=ADVANCED_BREP_SHAPE_REPRESENTATION ( '', ( #14083, #17681 ), #3818 ) ;
#15518=LINE ( 'NONE', #12822, #15330 ) ;
#15522=CARTESIAN_POINT ( 'NONE',  ( 1.800000000000000044, 11.40000000000000036, 7.550000000000000711 ) ) ;
#15547=DIRECTION ( 'NONE',  ( -2.220446049250309876E-16, -1.000000000000000000, -1.479114197289400113E-30 ) ) ;
#15548=FACE_OUTER_BOUND ( 'NONE', #13982, .T. ) ;
#15555=ORIENTED_EDGE ( 'NONE', *, *, #7807, .F. ) ;
#15557=DIRECTION ( 'NONE',  ( 1.000000000000000000, 1.776356839400250070E-15, 0.000000000000000000 ) ) ;
#15578=DIRECTION ( 'NONE',  ( 2.220446049250309876E-16, 1.000000000000000000, -5.551115123125800057E-15 ) ) ;
#15582=CARTESIAN_POINT ( 'NONE',  ( -1.899999999999999911, 0.5999999999999999778, 7.700000000000000178 ) ) ;
#15590=ORIENTED_EDGE ( 'NONE', *, *, #8897, .F. ) ;
#15601=ORIENTED_EDGE ( 'NONE', *, *, #8733, .T. ) ;
#15609=PLANE ( 'NONE',  #10527 ) ;
#15627=VECTOR ( 'NONE', #7980, 1000.000000000000000 ) ;
#15636=EDGE_CURVE ( 'NONE', #3897, #404, #15284, .T. ) ;
#15651=ORIENTED_EDGE ( 'NONE', *, *, #1618, .T. ) ;
#15654=VECTOR ( 'NONE', #13415, 1000.000000000000000 ) ;
#15655=ORIENTED_EDGE ( 'NONE', *, *, #9596, .T. ) ;
#15665=CARTESIAN_POINT ( 'NONE',  ( 1.750000000000000000, 0.5999999999999999778, 7.599999999999999645 ) ) ;
#15668=ORIENTED_EDGE ( 'NONE', *, *, #3121, .T. ) ;
#15669=DIRECTION ( 'NONE',  ( -2.220446049250309876E-16, -1.000000000000000000, 0.000000000000000000 ) ) ;
#15680=CARTESIAN_POINT ( 'NONE',  ( 1.899999999999999911, 11.40000000000000036, 7.550000000000000711 ) ) ;
#15682=DIRECTION ( 'NONE',  ( 1.000000000000000000, 0.000000000000000000, 0.000000000000000000 ) ) ;
#15687=CARTESIAN_POINT ( 'NONE',  ( -1.800000000000000044, 0.5999999999999999778, 6.599999999999999645 ) ) ;
#15695=ORIENTED_EDGE ( 'NONE', *, *, #5692, .T. ) ;
#15719=CARTESIAN_POINT ( 'NONE',  ( -0.5999999999999999778, 0.5999999999999999778, 7.599999999999999645 ) ) ;
#15720=VECTOR ( 'NONE', #12334, 1000.000000000000000 ) ;
#15746=CARTESIAN_POINT ( 'NONE',  ( 0.5999999999999999778, 0.5999999999999999778, 7.700000000000000178 ) ) ;
#15757=SURFACE_STYLE_USAGE ( .BOTH. , #7585 ) ;
#15773=CARTESIAN_POINT ( 'NONE',  ( 1.899999999999999911, 11.40000000000000036, 6.599999999999999645 ) ) ;
#15782=CARTESIAN_POINT ( 'NONE',  ( -0.5999999999999999778, 0.5999999999999999778, 7.700000000000000178 ) ) ;
#15802=LINE ( 'NONE', #4571, #11192 ) ;
#15810=ORIENTED_EDGE ( 'NONE', *, *, #10008, .F. ) ;
#15815=EDGE_CURVE ( 'NONE', #9659, #7174, #4332, .T. ) ;
#15829=DIRECTION ( 'NONE',  ( 1.850371707708589879E-16, 1.000000000000000000, 0.000000000000000000 ) ) ;
#15834=ORIENTED_EDGE ( 'NONE', *, *, #2350, .T. ) ;
#15836=ORIENTED_EDGE ( 'NONE', *, *, #1328, .F. ) ;
#15857=DIRECTION ( 'NONE',  ( 9.349246523159210481E-16, 0.000000000000000000, 1.000000000000000000 ) ) ;
#15859=AXIS2_PLACEMENT_3D ( 'NONE', #16468, #2499, #9617 ) ;
#15866=DIRECTION ( 'NONE',  ( 1.000000000000000000, -1.224646799147350002E-16, 0.000000000000000000 ) ) ;
#15867=CARTESIAN_POINT ( 'NONE',  ( 1.800000000000000044, 0.5999999999999999778, 6.599999999999999645 ) ) ;
#15870=CARTESIAN_POINT ( 'NONE',  ( 1.899999999999999911, 0.5999999999999999778, 7.550000000000000711 ) ) ;
#15887=VECTOR ( 'NONE', #16366, 1000.000000000000000 ) ;
#15889=COLOUR_RGB ( '', 0.31764706, 0.68627451, 0.89019608) ;
#15891=AXIS2_PLACEMENT_3D ( 'NONE', #3879, #2316, #9532 ) ;
#15905=VECTOR ( 'NONE', #6159, 1000.000000000000000 ) ;
#15906=AXIS2_PLACEMENT_3D ( 'NONE', #3484, #4969, #624 ) ;
#15919=VECTOR ( 'NONE', #1508, 1000.000000000000000 ) ;
#15926=CARTESIAN_POINT ( 'NONE',  ( -0.5999999999999999778, 0.5999999999999999778, 7.599999999999999645 ) ) ;
#15943=FILL_AREA_STYLE ('',( #295 ) ) ;
#15945=CARTESIAN_POINT ( 'NONE',  ( -1.149999999999999911, 9.299999999999998934, 7.500000000000000000 ) ) ;
#15962=ADVANCED_FACE ( 'NONE', ( #10808 ), #6637, .T. ) ;
#15967=ORIENTED_EDGE ( 'NONE', *, *, #3031, .F. ) ;
#15991=CYLINDRICAL_SURFACE ( 'NONE', #11802, 0.1999999999999996503 ) ;
#16012=DIRECTION ( 'NONE',  ( 9.349246523159200620E-16, 0.000000000000000000, -1.000000000000000000 ) ) ;
#16021=VERTEX_POINT ( 'NONE', #12390 ) ;
#16042=LINE ( 'NONE', #3341, #12079 ) ;
#16049=EDGE_LOOP ( 'NONE', ( #775, #2655, #7433, #3869 ) ) ;
#16053=CARTESIAN_POINT ( 'NONE',  ( 1.149999999999999911, 9.299999999999998934, 7.599999999999999645 ) ) ;
#16055=EDGE_CURVE ( 'NONE', #12172, #5374, #10718, .T. ) ;
#16063=ORIENTED_EDGE ( 'NONE', *, *, #7284, .F. ) ;
#16066=FACE_OUTER_BOUND ( 'NONE', #2703, .T. ) ;
#16067=VECTOR ( 'NONE', #9458, 1000.000000000000000 ) ;
#16072=AXIS2_PLACEMENT_3D ( 'NONE', #16079, #4682, #14590 ) ;
#16079=CARTESIAN_POINT ( 'NONE',  ( -1.149999999999999911, 6.472933199251450276, 6.846017351831609865 ) ) ;
#16083=ORIENTED_EDGE ( 'NONE', *, *, #5316, .F. ) ;
#16097=DIRECTION ( 'NONE',  ( -1.903239470785979823E-16, -1.000000000000000000, 0.000000000000000000 ) ) ;
#16104=DIRECTION ( 'NONE',  ( -1.000000000000000000, 0.000000000000000000, 0.000000000000000000 ) ) ;
#16108=LINE ( 'NONE', #3405, #13847 ) ;
#16109=( NAMED_UNIT ( * ) PLANE_ANGLE_UNIT ( ) SI_UNIT ( $, .RADIAN. ) );
#16111=DIRECTION ( 'NONE',  ( -1.000000000000000000, 2.220446049250309876E-16, 0.000000000000000000 ) ) ;
#16143=EDGE_CURVE ( 'NONE', #404, #2289, #5442, .T. ) ;
#16146=EDGE_CURVE ( 'NONE', #2289, #4403, #11272, .T. ) ;
#16159=VERTEX_POINT ( 'NONE', #5356 ) ;
#16166=EDGE_CURVE ( 'NONE', #10172, #13468, #8405, .T. ) ;
#16169=LINE ( 'NONE', #1997, #3198 ) ;
#16177=CARTESIAN_POINT ( 'NONE',  ( -1.300000000000000044, 1.592040838891560081E-16, 7.700000000000000178 ) ) ;
#16178=FACE_OUTER_BOUND ( 'NONE', #8603, .T. ) ;
#16181=DIRECTION ( 'NONE',  ( 1.000000000000000000, 4.433365283261159518E-17, 1.187916647401989926E-17 ) ) ;
#16189=FACE_OUTER_BOUND ( 'NONE', #6437, .T. ) ;
#16271=LINE ( 'NONE', #17629, #3478 ) ;
#16303=CARTESIAN_POINT ( 'NONE',  ( -0.5999999999999999778, 11.40000000000000036, 7.700000000000000178 ) ) ;
#16306=LINE ( 'NONE', #17767, #430 ) ;
#16314=SHAPE_DEFINITION_REPRESENTATION ( #1222, #2146 ) ;
#16322=ADVANCED_FACE ( 'NONE', ( #8854 ), #17171, .T. ) ;
#16335=CARTESIAN_POINT ( 'NONE',  ( -1.800000000000000044, 0.5999999999999999778, 7.550000000000000711 ) ) ;
#16366=DIRECTION ( 'NONE',  ( 3.700743415417190112E-16, 1.000000000000000000, 0.000000000000000000 ) ) ;
#16367=CARTESIAN_POINT ( 'NONE',  ( -0.9499999999999999556, 2.299999999999999822, 7.599999999999999645 ) ) ;
#16370=CARTESIAN_POINT ( 'NONE',  ( 1.699999999999999956, 2.299999999999999822, 7.700000000000000178 ) ) ;
#16402=VERTEX_POINT ( 'NONE', #10143 ) ;
#16435=AXIS2_PLACEMENT_3D ( 'NONE', #14524, #17378, #10788 ) ;
#16444=FACE_OUTER_BOUND ( 'NONE', #13192, .T. ) ;
#16460=CARTESIAN_POINT ( 'NONE',  ( -1.750000000000000000, 0.5999999999999999778, 7.599999999999999645 ) ) ;
#16468=CARTESIAN_POINT ( 'NONE',  ( -1.899999999999999911, 0.5999999999999999778, 7.599999999999999645 ) ) ;
#16469=CARTESIAN_POINT ( 'NONE',  ( -0.5999999999999999778, 10.80000000000000071, 7.599999999999999645 ) ) ;
#16488=EDGE_CURVE ( 'NONE', #11655, #14407, #3368, .T. ) ;
#16495=ORIENTED_EDGE ( 'NONE', *, *, #8445, .F. ) ;
#16497=VECTOR ( 'NONE', #14679, 1000.000000000000000 ) ;
#16505=VECTOR ( 'NONE', #15829, 1000.000000000000000 ) ;
#16519=LINE ( 'NONE', #9380, #1433 ) ;
#16532=VECTOR ( 'NONE', #10914, 1000.000000000000000 ) ;
#16543=CARTESIAN_POINT ( 'NONE',  ( 0.000000000000000000, 0.000000000000000000, 7.700000000000000178 ) ) ;
#16544=LINE ( 'NONE', #14773, #10656 ) ;
#16555=FACE_OUTER_BOUND ( 'NONE', #8179, .T. ) ;
#16584=DIRECTION ( 'NONE',  ( 0.000000000000000000, 0.000000000000000000, 1.000000000000000000 ) ) ;
#16596=CARTESIAN_POINT ( 'NONE',  ( 0.9499999999999999556, 2.299999999999999822, 7.700000000000000178 ) ) ;
#16603=CARTESIAN_POINT ( 'NONE',  ( 1.800000000000000044, 11.40000000000000036, 6.599999999999999645 ) ) ;
#16607=ORIENTED_EDGE ( 'NONE', *, *, #16055, .T. ) ;
#16622=CARTESIAN_POINT ( 'NONE',  ( 0.5999999999999999778, -7.347880794884110368E-17, 7.700000000000000178 ) ) ;
#16649=ORIENTED_EDGE ( 'NONE', *, *, #11069, .F. ) ;
#16658=DIRECTION ( 'NONE',  ( 1.850371707708589879E-16, 1.000000000000000000, 0.000000000000000000 ) ) ;
#16668=VECTOR ( 'NONE', #5293, 1000.000000000000000 ) ;
#16675=ORIENTED_EDGE ( 'NONE', *, *, #4729, .F. ) ;
#16681=DIRECTION ( 'NONE',  ( 0.000000000000000000, 0.000000000000000000, -1.000000000000000000 ) ) ;
#16682=CARTESIAN_POINT ( 'NONE',  ( -1.750000000000000000, 0.5999999999999999778, 7.550000000000000711 ) ) ;
#16705=DIRECTION ( 'NONE',  ( 8.269460797427580527E-16, 8.934339325041029556E-19, -1.000000000000000000 ) ) ;
#16707=EDGE_CURVE ( 'NONE', #616, #747, #3928, .T. ) ;
#16739=FACE_OUTER_BOUND ( 'NONE', #8256, .T. ) ;
#16747=LINE ( 'NONE', #6935, #11595 ) ;
#16762=LINE ( 'NONE', #9738, #6443 ) ;
#16766=LINE ( 'NONE', #1401, #5257 ) ;
#16767=( GEOMETRIC_REPRESENTATION_CONTEXT ( 3 ) GLOBAL_UNCERTAINTY_ASSIGNED_CONTEXT ( ( #2701 ) ) GLOBAL_UNIT_ASSIGNED_CONTEXT ( ( #6020, #16109, #381 ) ) REPRESENTATION_CONTEXT ( 'NONE', 'WORKASPACE' ) );
#16771=DIRECTION ( 'NONE',  ( -1.000000000000000000, 0.000000000000000000, 0.000000000000000000 ) ) ;
#16779=VERTEX_POINT ( 'NONE', #15522 ) ;
#16792=CIRCLE ( 'NONE', #8220, 0.1999999999999998168 ) ;
#16804=PLANE ( 'NONE',  #7044 ) ;
#16811=CIRCLE ( 'NONE', #1736, 0.9499999999999999556 ) ;
#16825=EDGE_CURVE ( 'NONE', #84, #6428, #8298, .T. ) ;
#16836=DIRECTION ( 'NONE',  ( 0.000000000000000000, 0.000000000000000000, 1.000000000000000000 ) ) ;
#16849=CARTESIAN_POINT ( 'NONE',  ( 1.800000000000000044, 0.5999999999999999778, 7.550000000000000711 ) ) ;
#16867=LINE ( 'NONE', #8272, #169 ) ;
#16869=DIRECTION ( 'NONE',  ( -1.048990684667790150E-15, 0.000000000000000000, -1.000000000000000000 ) ) ;
#16874=ORIENTED_EDGE ( 'NONE', *, *, #148, .F. ) ;
#16885=VECTOR ( 'NONE', #13298, 1000.000000000000114 ) ;
#16893=CARTESIAN_POINT ( 'NONE',  ( 1.149999999999999911, 9.248236190979499227, 7.693185165257809821 ) ) ;
#16909=CARTESIAN_POINT ( 'NONE',  ( 0.5999999999999999778, 10.80000000000000071, 7.599999999999999645 ) ) ;
#16919=CARTESIAN_POINT ( 'NONE',  ( -0.2749999999999995781, 2.299999999999999822, 7.599999999999999645 ) ) ;
#16926=EDGE_LOOP ( 'NONE', ( #13778, #10477, #16649, #15967 ) ) ;
#16944=EDGE_CURVE ( 'NONE', #13978, #15121, #7361, .T. ) ;
#16950=CARTESIAN_POINT ( 'NONE',  ( -1.800000000000000044, 11.40000000000000036, 6.599999999999999645 ) ) ;
#16974=ORIENTED_EDGE ( 'NONE', *, *, #4407, .F. ) ;
#16986=ORIENTED_EDGE ( 'NONE', *, *, #14183, .T. ) ;
#16996=DIRECTION ( 'NONE',  ( 0.000000000000000000, 0.000000000000000000, 1.000000000000000000 ) ) ;
#17019=LINE ( 'NONE', #3130, #6146 ) ;
#17030=CARTESIAN_POINT ( 'NONE',  ( 4.225031457058369810E-16, 2.299999999999999822, 7.700000000000000178 ) ) ;
#17059=DIRECTION ( 'NONE',  ( -0.000000000000000000, 1.000000000000000000, 0.000000000000000000 ) ) ;
#17064=ORIENTED_EDGE ( 'NONE', *, *, #2379, .T. ) ;
#17066=VECTOR ( 'NONE', #14428, 1000.000000000000000 ) ;
#17077=CARTESIAN_POINT ( 'NONE',  ( -0.5999999999999999778, 10.80000000000000071, 7.700000000000000178 ) ) ;
#17082=VECTOR ( 'NONE', #8770, 1000.000000000000000 ) ;
#17104=CARTESIAN_POINT ( 'NONE',  ( -1.750000000000000000, 0.5999999999999999778, 7.700000000000000178 ) ) ;
#17107=EDGE_CURVE ( 'NONE', #16021, #9457, #5338, .T. ) ;
#17124=DIRECTION ( 'NONE',  ( -1.000000000000000000, 0.000000000000000000, 0.000000000000000000 ) ) ;
#17137=ORIENTED_EDGE ( 'NONE', *, *, #3511, .T. ) ;
#17138=LINE ( 'NONE', #15773, #3789 ) ;
#17150=VERTEX_POINT ( 'NONE', #5233 ) ;
#17158=DIRECTION ( 'NONE',  ( -1.000000000000000000, 0.000000000000000000, 0.000000000000000000 ) ) ;
#17171=PLANE ( 'NONE',  #1709 ) ;
#17184=ORIENTED_EDGE ( 'NONE', *, *, #9286, .F. ) ;
#17186=FACE_OUTER_BOUND ( 'NONE', #13527, .T. ) ;
#17191=FACE_OUTER_BOUND ( 'NONE', #7053, .T. ) ;
#17194=DIRECTION ( 'NONE',  ( -1.850371707708589879E-16, -1.000000000000000000, 0.000000000000000000 ) ) ;
#17196=EDGE_LOOP ( 'NONE', ( #3771, #14003, #15436, #6011 ) ) ;
#17224=ORIENTED_EDGE ( 'NONE', *, *, #8684, .F. ) ;
#17226=CARTESIAN_POINT ( 'NONE',  ( 0.5999999999999999778, -7.347880794884110368E-17, 7.599999999999999645 ) ) ;
#17233=ORIENTED_EDGE ( 'NONE', *, *, #324, .F. ) ;
#17235=DIRECTION ( 'NONE',  ( 0.000000000000000000, 0.000000000000000000, 1.000000000000000000 ) ) ;
#17252=EDGE_LOOP ( 'NONE', ( #3829, #6382, #12849, #15836 ) ) ;
#17256=ADVANCED_FACE ( 'NONE', ( #11255 ), #16804, .F. ) ;
#17263=CARTESIAN_POINT ( 'NONE',  ( -1.149999999999999911, 6.472933199251450276, 6.846017351831609865 ) ) ;
#17268=DIRECTION ( 'NONE',  ( -1.000000000000000000, 0.000000000000000000, 0.000000000000000000 ) ) ;
#17282=LINE ( 'NONE', #12965, #10907 ) ;
#17286=DIRECTION ( 'NONE',  ( 2.220446049250319983E-16, 1.000000000000000000, -2.047034224795619731E-16 ) ) ;
#17307=ORIENTED_EDGE ( 'NONE', *, *, #4273, .T. ) ;
#17314=VECTOR ( 'NONE', #9097, 1000.000000000000000 ) ;
#17315=DIRECTION ( 'NONE',  ( -1.445602896647339508E-15, 0.000000000000000000, 1.000000000000000000 ) ) ;
#17329=ORIENTED_EDGE ( 'NONE', *, *, #7284, .T. ) ;
#17330=AXIS2_PLACEMENT_3D ( 'NONE', #10443, #9147, #16104 ) ;
#17340=AXIS2_PLACEMENT_3D ( 'NONE', #5914, #13213, #8957 ) ;
#17353=PLANE ( 'NONE',  #16072 ) ;
#17361=DIRECTION ( 'NONE',  ( 0.000000000000000000, 0.000000000000000000, 1.000000000000000000 ) ) ;
#17362=VERTEX_POINT ( 'NONE', #5703 ) ;
#17364=AXIS2_PLACEMENT_3D ( 'NONE', #8294, #1250, #5223 ) ;
#17369=CARTESIAN_POINT ( 'NONE',  ( 1.149999999999999911, 9.299999999999998934, 7.700000000000000178 ) ) ;
#17370=LINE ( 'NONE', #13039, #7327 ) ;
#17373=CIRCLE ( 'NONE', #17922, 0.1499999999999999667 ) ;
#17378=DIRECTION ( 'NONE',  ( 0.000000000000000000, 0.000000000000000000, 1.000000000000000000 ) ) ;
#17385=ORIENTED_EDGE ( 'NONE', *, *, #9516, .F. ) ;
#17396=EDGE_CURVE ( 'NONE', #7108, #3985, #14878, .T. ) ;
#17427=EDGE_LOOP ( 'NONE', ( #8920, #4025, #7856, #1812 ) ) ;
#17443=CIRCLE ( 'NONE', #5658, 0.04999999999999991257 ) ;
#17448=DIRECTION ( 'NONE',  ( 1.000000000000000000, 0.000000000000000000, 0.000000000000000000 ) ) ;
#17451=ORIENTED_EDGE ( 'NONE', *, *, #12740, .T. ) ;
#17460=CARTESIAN_POINT ( 'NONE',  ( -1.899999999999999911, 0.5999999999999999778, 7.599999999999999645 ) ) ;
#17467=DIRECTION ( 'NONE',  ( -1.000000000000000000, 1.850371707708589879E-16, 0.000000000000000000 ) ) ;
#17471=EDGE_CURVE ( 'NONE', #2611, #4443, #16169, .T. ) ;
#17485=FACE_OUTER_BOUND ( 'NONE', #3995, .T. ) ;
#17486=EDGE_LOOP ( 'NONE', ( #7982, #12539, #1304, #18011 ) ) ;
#17522=ORIENTED_EDGE ( 'NONE', *, *, #2064, .T. ) ;
#17524=ADVANCED_FACE ( 'NONE', ( #8039 ), #618, .F. ) ;
#17548=CARTESIAN_POINT ( 'NONE',  ( -1.800000000000000044, 0.5999999999999999778, 6.599999999999999645 ) ) ;
#17554=CARTESIAN_POINT ( 'NONE',  ( -1.300000000000000044, 1.592040838891560081E-16, 7.599999999999999645 ) ) ;
#17574=CARTESIAN_POINT ( 'NONE',  ( 1.899999999999999911, 11.40000000000000036, 7.550000000000000711 ) ) ;
#17576=VERTEX_POINT ( 'NONE', #17905 ) ;
#17583=ORIENTED_EDGE ( 'NONE', *, *, #17471, .T. ) ;
#17587=ORIENTED_EDGE ( 'NONE', *, *, #2379, .F. ) ;
#17602=CIRCLE ( 'NONE', #3146, 0.04999999999999969746 ) ;
#17604=DIRECTION ( 'NONE',  ( -2.055968564120659776E-16, -1.000000000000000000, 0.000000000000000000 ) ) ;
#17609=CARTESIAN_POINT ( 'NONE',  ( 0.000000000000000000, 0.000000000000000000, 7.599999999999999645 ) ) ;
#17629=CARTESIAN_POINT ( 'NONE',  ( 1.800000000000000044, 11.40000000000000036, 6.599999999999999645 ) ) ;
#17630=LINE ( 'NONE', #7950, #6375 ) ;
#17631=AXIS2_PLACEMENT_3D ( 'NONE', #12159, #16681, #1135 ) ;
#17650=LINE ( 'NONE', #17554, #15654 ) ;
#17671=ORIENTED_EDGE ( 'NONE', *, *, #18172, .F. ) ;
#17680=DIRECTION ( 'NONE',  ( -5.551115123125880521E-15, 1.000000000000000000, 6.055990775824630636E-30 ) ) ;
#17681=AXIS2_PLACEMENT_3D ( 'NONE', #11191, #16836, #4146 ) ;
#17688=AXIS2_PLACEMENT_3D ( 'NONE', #6612, #9103, #688 ) ;
#17701=AXIS2_PLACEMENT_3D ( 'NONE', #1318, #6965, #2997 ) ;
#17704=CARTESIAN_POINT ( 'NONE',  ( 1.750000000000000000, 11.40000000000000036, 7.700000000000000178 ) ) ;
#17711=CARTESIAN_POINT ( 'NONE',  ( 1.800000000000000044, 0.5999999999999999778, 6.599999999999999645 ) ) ;
#17718=DIRECTION ( 'NONE',  ( 0.000000000000000000, 0.000000000000000000, 1.000000000000000000 ) ) ;
#17749=EDGE_CURVE ( 'NONE', #11926, #2448, #16519, .T. ) ;
#17751=CARTESIAN_POINT ( 'NONE',  ( -0.5999999999999999778, 7.347880794884128857E-17, 7.599999999999999645 ) ) ;
#17753=FACE_OUTER_BOUND ( 'NONE', #13087, .T. ) ;
#17766=EDGE_CURVE ( 'NONE', #6049, #13978, #12256, .T. ) ;
#17767=CARTESIAN_POINT ( 'NONE',  ( -0.5999999999999999778, 11.40000000000000036, 7.599999999999999645 ) ) ;
#17776=CARTESIAN_POINT ( 'NONE',  ( 0.9499999999999999556, 2.299999999999999822, 7.700000000000000178 ) ) ;
#17871=ORIENTED_EDGE ( 'NONE', *, *, #1328, .T. ) ;
#17899=FACE_BOUND ( 'NONE', #10305, .T. ) ;
#17905=CARTESIAN_POINT ( 'NONE',  ( 1.300000000000000044, -1.592040838891560081E-16, 7.599999999999999645 ) ) ;
#17922=AXIS2_PLACEMENT_3D ( 'NONE', #16682, #15578, #11400 ) ;
#17923=CARTESIAN_POINT ( 'NONE',  ( -1.800000000000000044, 11.40000000000000036, 7.550000000000000711 ) ) ;
#17956=EDGE_CURVE ( 'NONE', #12938, #2115, #16811, .T. ) ;
#17974=VECTOR ( 'NONE', #13782, 1000.000000000000000 ) ;
#17989=EDGE_CURVE ( 'NONE', #4730, #7436, #17138, .T. ) ;
#17996=CARTESIAN_POINT ( 'NONE',  ( -1.800000000000000044, 0.5999999999999999778, 7.550000000000000711 ) ) ;
#18011=ORIENTED_EDGE ( 'NONE', *, *, #12083, .F. ) ;
#18038=AXIS2_PLACEMENT_3D ( 'NONE', #15080, #8208, #15251 ) ;
#18071=CARTESIAN_POINT ( 'NONE',  ( -1.899999999999999911, 0.5999999999999999778, 7.599999999999999645 ) ) ;
#18142=DIRECTION ( 'NONE',  ( -1.000000000000000000, 0.000000000000000000, 0.000000000000000000 ) ) ;
#18169=EDGE_CURVE ( 'NONE', #16021, #12172, #16042, .T. ) ;
#18172=EDGE_CURVE ( 'NONE', #1173, #10172, #11873, .T. ) ;
#18177=VECTOR ( 'NONE', #7913, 1000.000000000000000 ) ;
#18183=DIRECTION ( 'NONE',  ( 2.220446049250309876E-16, 1.000000000000000000, 0.000000000000000000 ) ) ;
#18184=CARTESIAN_POINT ( 'NONE',  ( -1.149999999999999911, 9.248236190979499227, 7.693185165257809821 ) ) ;
#18188=ORIENTED_EDGE ( 'NONE', *, *, #5878, .T. ) ;
#18191=CARTESIAN_POINT ( 'NONE',  ( -1.800000000000000044, 11.40000000000000036, 6.599999999999999645 ) ) ;
#18198=DIRECTION ( 'NONE',  ( 1.000000000000000000, -1.850371707708589879E-16, 0.000000000000000000 ) ) ;
#18221=VECTOR ( 'NONE', #1273, 1000.000000000000000 ) ;
#18224=PLANE ( 'NONE',  #7311 ) ;
#18248=AXIS2_PLACEMENT_3D ( 'NONE', #1565, #271, #5729 ) ;
#18252=ADVANCED_FACE ( 'NONE', ( #6121 ), #11785, .T. ) ;
#18256=CARTESIAN_POINT ( 'NONE',  ( 1.300000000000000044, -1.592040838891560081E-16, 7.599999999999999645 ) ) ;
#18280=VECTOR ( 'NONE', #15682, 1000.000000000000000 ) ;
ENDSEC;
END-ISO-10303-21;
